ISO-10303-21;
HEADER;
FILE_DESCRIPTION (('STEP AP203'),
    '1' );
FILE_NAME ('Part7_handle1Sleeve.step',
    '2026-10-06T15:07:10',
    ( '' ),
    ( '' ),
    'SwSTEP 2.0',
    'SolidWorks 2024',
    '' );
FILE_SCHEMA (( 'AUTOMOTIVE_DESIGN' ));
ENDSEC;

DATA;
#2=CARTESIAN_POINT ( 'NONE',  ( 54.89716490668163118, -3.628845007888942931, 0.07017451552782483226 ) ) ;
#10=CARTESIAN_POINT ( 'NONE',  ( 18.75828436641558028, -5.879118399717574661, -3.993434336035625254 ) ) ;
#17=CARTESIAN_POINT ( 'NONE',  ( 69.01456695820279208, -4.997110861600952525, -4.033870539711066350 ) ) ;
#68=EDGE_LOOP ( 'NONE', ( #22629, #18065, #11744, #10106 ) ) ;
#86=CARTESIAN_POINT ( 'NONE',  ( 101.9216173105994159, -5.769792427975438898, -0.07017451552783579571 ) ) ;
#88=CARTESIAN_POINT ( 'NONE',  ( 54.64624227588102201, -3.635739347938791610, 0.02339150516273077324 ) ) ;
#101=CARTESIAN_POINT ( 'NONE',  ( 18.76371685221734964, -5.818394111045739336, -4.091315477141358237 ) ) ;
#155=CARTESIAN_POINT ( 'NONE',  ( 85.03119751210560651, -5.129410398413424055, 4.093303008813728994 ) ) ;
#189=CARTESIAN_POINT ( 'NONE',  ( 102.9885081044300534, -6.698322160490901567, -0.07017451552781736601 ) ) ;
#198=CARTESIAN_POINT ( 'NONE',  ( 28.66386174151161370, -4.482150724175043344, 2.184956778824117762 ) ) ;
#202=B_SPLINE_CURVE_WITH_KNOTS ( 'NONE', 3,
 ( #27500, #19992, #25480, #30192, #2590, #12755, #27322, #4443 ),
 .UNSPECIFIED., .F., .F.,
 ( 4, 2, 2, 4 ),
 ( 0.000000000000000000, 0.5000000000000000000, 0.7500000000000000000, 1.000000000000000000 ),
 .UNSPECIFIED. ) ;
#205=CARTESIAN_POINT ( 'NONE',  ( 101.9216173105994443, -5.769792427975428240, -0.07017451552783622593 ) ) ;
#209=DIRECTION ( 'NONE',  ( -0.9975973382524639943, -0.06927878976713693071, 0.000000000000000000 ) ) ;
#210=CARTESIAN_POINT ( 'NONE',  ( 40.87780399789884456, -5.761808403395388467, -4.013697493846343889 ) ) ;
#238=CARTESIAN_POINT ( 'NONE',  ( 18.75828436641558028, -5.879118399717575549, 3.993434336035622589 ) ) ;
#256=VERTEX_POINT ( 'NONE', #8036 ) ;
#262=CARTESIAN_POINT ( 'NONE',  ( 102.9885081044300534, -6.698322160490901567, 0.07017451552781736601 ) ) ;
#275=CARTESIAN_POINT ( 'NONE',  ( 18.80941384712784981, -5.307593421039076276, 3.636029349014984202 ) ) ;
#278=CARTESIAN_POINT ( 'NONE',  ( 69.22368686548678340, -4.843077221807417843, 5.695980980372492120 ) ) ;
#289=CARTESIAN_POINT ( 'NONE',  ( 19.10390797508229710, -2.015740111943975066, -0.07017451552781585333 ) ) ;
#300=CARTESIAN_POINT ( 'NONE',  ( 48.09670199522224721, -9.430894477034977186, 0.07017451552781803215 ) ) ;
#322=CARTESIAN_POINT ( 'NONE',  ( 102.2656009641821271, -1.731193774301692523, -2.184956770134436344 ) ) ;
#326=CARTESIAN_POINT ( 'NONE',  ( 28.66745692012980840, -6.633544308268587208, 4.150065909475219250 ) ) ;
#349=CARTESIAN_POINT ( 'NONE',  ( 29.27523314209411609, -3.695744416148339706, -0.07017451552781629742 ) ) ;
#360=CARTESIAN_POINT ( 'NONE',  ( 28.68200330690814681, -6.065191176915236682, -4.312042181581901445 ) ) ;
#376=CARTESIAN_POINT ( 'NONE',  ( 18.60402535541760827, -7.603424548860325594, -0.4426577273443823568 ) ) ;
#392=EDGE_CURVE ( 'NONE', #27444, #8159, #6302, .T. ) ;
#394=CARTESIAN_POINT ( 'NONE',  ( 18.65837979360809840, -6.995851018290569989, 0.07017451552783667001 ) ) ;
#413=CARTESIAN_POINT ( 'NONE',  ( 101.6441386174529953, -1.774168274679931212, 2.184956718805492581 ) ) ;
#424=LINE ( 'NONE', #31348, #31150 ) ;
#433=CARTESIAN_POINT ( 'NONE',  ( 47.98568197278773795, -2.821418575600917578, -1.010822989962086416 ) ) ;
#443=CARTESIAN_POINT ( 'NONE',  ( 85.48138648428258080, -7.654866896025229295, 1.915219082070893863 ) ) ;
#452=CARTESIAN_POINT ( 'NONE',  ( 41.35542541871918587, -7.892720653449311285, -2.184957211333078408 ) ) ;
#468=CARTESIAN_POINT ( 'NONE',  ( 54.93487251133846883, -4.984033517864898677, -3.390608480941980307 ) ) ;
#472=CARTESIAN_POINT ( 'NONE',  ( 18.77392604112944596, -5.704275868917796366, 4.185347664740951323 ) ) ;
#476=ORIENTED_EDGE ( 'NONE', *, *, #29164, .F. ) ;
#484=CARTESIAN_POINT ( 'NONE',  ( 18.72482702355275919, -6.253104344970715545, -3.390608483633605896 ) ) ;
#496=CARTESIAN_POINT ( 'NONE',  ( 35.27105150273526135, -8.350847396885011875, 0.8105616794655192692 ) ) ;
#507=CARTESIAN_POINT ( 'NONE',  ( 69.02940965804741325, -5.294544073343872448, -4.275175994953113623 ) ) ;
#513=CARTESIAN_POINT ( 'NONE',  ( 48.09670199522225431, -9.430894477034977186, -1.010822989962099960 ) ) ;
#518=CARTESIAN_POINT ( 'NONE',  ( 28.57616583553759426, -7.888378049842258655, 2.184956778784801212 ) ) ;
#525=PLANE ( 'NONE',  #17308 ) ;
#554=CARTESIAN_POINT ( 'NONE',  ( 18.90256931246762662, -4.266302279389236674, 3.236220886658451867 ) ) ;
#566=CARTESIAN_POINT ( 'NONE',  ( 102.4497391607695107, -4.374320780259970398, 3.390608474976775533 ) ) ;
#576=CARTESIAN_POINT ( 'NONE',  ( 85.13613392229180477, -2.069934983084472879, 2.713652344655542503 ) ) ;
#586=CARTESIAN_POINT ( 'NONE',  ( 29.41391112839825794, -2.700987858898180161, -0.07017451552781628354 ) ) ;
#610=CARTESIAN_POINT ( 'NONE',  ( 85.12704628545870378, -6.675959057340966396, -1.529339193924102558 ) ) ;
#638=CARTESIAN_POINT ( 'NONE',  ( 85.03224897449447894, -5.146568951867915409, 4.073740955748646364 ) ) ;
#653=B_SPLINE_SURFACE_WITH_KNOTS ( 'NONE', 3, 3, ( 
 ( #5901, #17970, #28158, #18296, #756, #15621, #31007, #8088, #16091, #15434 ),
 ( #25834, #26324, #2957, #28315, #10939, #23314, #28505, #26145, #3102, #23459 ),
 ( #566, #10757, #21141, #31191, #8273, #19272, #9234, #8753, #18779, #9052 ),
 ( #6575, #23945, #11248, #16772, #29297, #26626, #28989, #23798, #911, #19109 ) ),
 .UNSPECIFIED., .F., .F., .F.,
 ( 4, 4 ),
 ( 4, 3, 3, 4 ),
 ( -1.565413741823433983E-11, 1.000000000000000444 ),
 ( 0.003584360682152736184, 0.5017921803410764214, 0.7508960901705381552, 1.000000000000000000 ),
 .UNSPECIFIED. ) ;
#656=CARTESIAN_POINT ( 'NONE',  ( 29.21679767122667570, -7.327048195454283430, -2.787782193710479195 ) ) ;
#670=CARTESIAN_POINT ( 'NONE',  ( 19.01480233880980819, -3.011762293215293429, -0.07017451552781921176 ) ) ;
#672=CARTESIAN_POINT ( 'NONE',  ( 23.62103335626344958, -7.897478826046258504, 1.169950778987780771 ) ) ;
#679=CARTESIAN_POINT ( 'NONE',  ( 41.43709133142961321, -4.769546740945156849, 4.522129901861162260 ) ) ;
#687=CARTESIAN_POINT ( 'NONE',  ( 54.94807382917689154, -5.453310457255624577, -4.112224493141035886 ) ) ;
#718=VECTOR ( 'NONE', #3334, 1000.000000000000000 ) ;
#723=CARTESIAN_POINT ( 'NONE',  ( 40.74410603220335503, -8.021703207526138968, -2.184955501622229068 ) ) ;
#724=CARTESIAN_POINT ( 'NONE',  ( 101.9216173105994443, -5.769792427975428240, -0.07017451552783622593 ) ) ;
#727=ORIENTED_EDGE ( 'NONE', *, *, #28371, .F. ) ;
#735=FACE_OUTER_BOUND ( 'NONE', #6838, .T. ) ;
#756=CARTESIAN_POINT ( 'NONE',  ( 47.94941403272063951, -7.827919050483855834, 2.184956529741820752 ) ) ;
#786=CARTESIAN_POINT ( 'NONE',  ( 102.2339617642410872, -1.281710854344942918, -1.169950773171123615 ) ) ;
#806=CARTESIAN_POINT ( 'NONE',  ( 40.87351160865108568, -4.997573076398440506, 2.787782134468652639 ) ) ;
#816=CARTESIAN_POINT ( 'NONE',  ( 18.96091535642496240, -3.614110606601104614, -2.184956778830005053 ) ) ;
#821=CARTESIAN_POINT ( 'NONE',  ( 69.03558484035113452, -5.418257723523708158, 4.312042181588143563 ) ) ;
#855=CARTESIAN_POINT ( 'NONE',  ( 40.88398074938778137, -6.894607256478876955, 3.996604168373521837 ) ) ;
#859=ORIENTED_EDGE ( 'NONE', *, *, #4261, .T. ) ;
#887=CARTESIAN_POINT ( 'NONE',  ( 101.8797206818349821, -5.166491396337139719, -2.184956718990371805 ) ) ;
#898=CARTESIAN_POINT ( 'NONE',  ( 69.38611993481310947, -8.080330187063884395, -2.713652344655543391 ) ) ;
#911=CARTESIAN_POINT ( 'NONE',  ( 23.71121667297767388, -6.322215142808032873, 3.993434336039484833 ) ) ;
#922=EDGE_CURVE ( 'NONE', #4124, #22902, #28033, .T. ) ;
#929=B_SPLINE_SURFACE_WITH_KNOTS ( 'NONE', 1, 3, ( 
 ( #24414, #9994, #24573, #16743, #11708, #9375, #1887, #1698 ),
 ( #20370, #7474, #25388, #21910, #20206, #4373, #33072, #9205 ) ),
 .UNSPECIFIED., .F., .F., .F.,
 ( 2, 2 ),
 ( 4, 2, 2, 4 ),
 ( 0.000000000000000000, 1.000000000000000000 ),
 ( 0.000000000000000000, 0.5000000000000000000, 0.7500000000000000000, 1.000000000000000000 ),
 .UNSPECIFIED. ) ;
#935=LINE ( 'NONE', #25672, #31041 ) ;
#936=CARTESIAN_POINT ( 'NONE',  ( 102.2410647596622937, -1.384237843926474643, -1.529339869963366683 ) ) ;
#945=CARTESIAN_POINT ( 'NONE',  ( 102.5401559989745266, -5.675509796544895735, -0.8105616764226521997 ) ) ;
#964=CARTESIAN_POINT ( 'NONE',  ( 18.79826502154066148, -5.432214915678442502, 4.312042181580753031 ) ) ;
#970=CARTESIAN_POINT ( 'NONE',  ( 18.84751267742354841, -4.881724961800174789, 4.171847256157207084 ) ) ;
#978=CARTESIAN_POINT ( 'NONE',  ( 69.10820754288535284, -6.866680491174807166, -2.787783121313799128 ) ) ;
#992=CARTESIAN_POINT ( 'NONE',  ( 47.94950013216585916, -7.827917879355857700, 2.184956529945685233 ) ) ;
#998=CARTESIAN_POINT ( 'NONE',  ( 102.4231258375787661, -3.997392187481084047, 3.997238528708670913 ) ) ;
#1122=CARTESIAN_POINT ( 'NONE',  ( 28.69034050020728799, -5.741730000312176507, 4.155404940063129438 ) ) ;
#1149=CARTESIAN_POINT ( 'NONE',  ( 29.35001421184127324, -4.582605737176274729, 4.522129901861162260 ) ) ;
#1158=CARTESIAN_POINT ( 'NONE',  ( 18.65791233782715963, -7.001076235476726417, 2.184956778830005941 ) ) ;
#1159=VERTEX_POINT ( 'NONE', #3799 ) ;
#1165=CARTESIAN_POINT ( 'NONE',  ( 40.88399151329760883, -6.896594116963963295, 3.993433839888539172 ) ) ;
#1194=CARTESIAN_POINT ( 'NONE',  ( 18.71626227658832065, -6.348841026559134626, -3.236291062301399180 ) ) ;
#1217=CARTESIAN_POINT ( 'NONE',  ( 40.87773744809802423, -5.749688186340451423, -3.995006151633446745 ) ) ;
#1220=CARTESIAN_POINT ( 'NONE',  ( 28.63490450844110313, -5.610497434542901729, 3.993434336046763899 ) ) ;
#1275=CARTESIAN_POINT ( 'NONE',  ( 19.01480233880980819, -3.011762293215292097, -0.4367666033480814836 ) ) ;
#1293=PRODUCT_DEFINITION_FORMATION_WITH_SPECIFIED_SOURCE ( 'ANY', '', #30333, .NOT_KNOWN. ) ;
#1312=CARTESIAN_POINT ( 'NONE',  ( 18.82056267271149252, -5.182971926439480015, 4.312042181588143563 ) ) ;
#1314=CARTESIAN_POINT ( 'NONE',  ( 84.99303864846685030, -4.506833362023316525, -4.312042181581901445 ) ) ;
#1325=CARTESIAN_POINT ( 'NONE',  ( 47.98568197278775216, -2.821418575600922019, -0.07017451552781628354 ) ) ;
#1346=VERTEX_POINT ( 'NONE', #30372 ) ;
#1348=CARTESIAN_POINT ( 'NONE',  ( 69.07041625887113412, -6.115693503127433317, 3.994703126862036324 ) ) ;
#1387=CARTESIAN_POINT ( 'NONE',  ( 84.96562648226598924, -4.059759578883751274, -3.994701829040198326 ) ) ;
#1406=CARTESIAN_POINT ( 'NONE',  ( 48.06508596181272708, -7.548662730768715079, -4.522129901861164036 ) ) ;
#1426=B_SPLINE_CURVE_WITH_KNOTS ( 'NONE', 3,
 ( #20510, #30720, #28173, #15639, #15450, #586, #10777, #8106 ),
 .UNSPECIFIED., .F., .F.,
 ( 4, 2, 2, 4 ),
 ( 0.000000000000000000, 0.5000000000000000000, 0.7500000000000000000, 1.000000000000000000 ),
 .UNSPECIFIED. ) ;
#1438=CARTESIAN_POINT ( 'NONE',  ( 102.5437075123492292, -5.726773290143884587, -0.4367666012718967594 ) ) ;
#1442=LINE ( 'NONE', #27158, #17729 ) ;
#1451=CARTESIAN_POINT ( 'NONE',  ( 28.63490450844348345, -5.610497434546049433, -3.993434336023980791 ) ) ;
#1460=CARTESIAN_POINT ( 'NONE',  ( 28.67239840559724584, -6.439901994837876842, 4.275175838841350995 ) ) ;
#1464=CARTESIAN_POINT ( 'NONE',  ( 40.87805050009787067, -5.806737366949438872, -4.073741263089366349 ) ) ;
#1475=CARTESIAN_POINT ( 'NONE',  ( 23.95058674323790271, -2.449331254364353949, -0.07017451552781628354 ) ) ;
#1479=EDGE_CURVE ( 'NONE', #256, #2205, #935, .T. ) ;
#1489=CARTESIAN_POINT ( 'NONE',  ( 23.84310522038038727, -4.329614468550014195, -4.522129901861162260 ) ) ;
#1496=FACE_OUTER_BOUND ( 'NONE', #16801, .T. ) ;
#1511=CARTESIAN_POINT ( 'NONE',  ( 19.10390797508229710, -2.015740111943975066, 0.07017451552782062729 ) ) ;
#1525=CARTESIAN_POINT ( 'NONE',  ( 68.93909985284442143, -3.497255374392779448, 1.529340295389710169 ) ) ;
#1538=CARTESIAN_POINT ( 'NONE',  ( 54.94558419843593100, -5.363357418298841495, -3.999773680160701783 ) ) ;
#1569=CARTESIAN_POINT ( 'NONE',  ( 69.13057415542957074, -2.987362752442195291, -2.713652344655540727 ) ) ;
#1572=EDGE_LOOP ( 'NONE', ( #30390, #4020, #23354, #26459 ) ) ;
#1573=ORIENTED_EDGE ( 'NONE', *, *, #19612, .F. ) ;
#1585=CARTESIAN_POINT ( 'NONE',  ( 101.8405149130903027, -4.601938079581686658, 3.093519980324558549 ) ) ;
#1615=CARTESIAN_POINT ( 'NONE',  ( 69.05424452633151589, -5.791958783353122087, -4.275175994963405834 ) ) ;
#1625=CARTESIAN_POINT ( 'NONE',  ( 18.91888895626146905, -4.083881414823423484, -2.942177715856218789 ) ) ;
#1628=ORIENTED_EDGE ( 'NONE', *, *, #28715, .T. ) ;
#1631=CARTESIAN_POINT ( 'NONE',  ( 85.08949032934708612, -1.315411135598755221, -0.07017451552781628354 ) ) ;
#1651=CARTESIAN_POINT ( 'NONE',  ( 47.95270804829356592, -8.021719045401216164, 1.873788950397360820 ) ) ;
#1657=CARTESIAN_POINT ( 'NONE',  ( 85.03478631109508967, -5.187975910970339832, 4.018749453427868268 ) ) ;
#1690=CARTESIAN_POINT ( 'NONE',  ( 29.33517104211142268, -3.852857368063845822, 1.169950485891758429 ) ) ;
#1693=CARTESIAN_POINT ( 'NONE',  ( 69.42401195566041849, -8.835509274224046194, -0.07017451552783579571 ) ) ;
#1698=CARTESIAN_POINT ( 'NONE',  ( 19.03654924710325602, -2.768675503676416572, -2.713652344655542503 ) ) ;
#1708=CARTESIAN_POINT ( 'NONE',  ( 28.69357983231036613, -5.616541217350277115, -3.994702635790153167 ) ) ;
#1713=CARTESIAN_POINT ( 'NONE',  ( 85.08949032934707191, -1.315411135598753445, 1.010822989962091301 ) ) ;
#1762=CARTESIAN_POINT ( 'NONE',  ( 102.5305753040692878, -0.1042037546421146210, -0.07017451552781628354 ) ) ;
#1763=ORIENTED_EDGE ( 'NONE', *, *, #19526, .T. ) ;
#1771=CARTESIAN_POINT ( 'NONE',  ( 23.61221640758335027, -8.051464822112823327, -0.4367666033548386340 ) ) ;
#1804=CARTESIAN_POINT ( 'NONE',  ( 102.4008411508948768, -3.675699656443788044, -4.275175836096084758 ) ) ;
#1835=CARTESIAN_POINT ( 'NONE',  ( 101.6441386174529953, -1.774168274679931212, 2.184956718805492581 ) ) ;
#1837=CARTESIAN_POINT ( 'NONE',  ( 69.18703749905368738, -4.112663945007549060, -4.522129901861162260 ) ) ;
#1847=CARTESIAN_POINT ( 'NONE',  ( 28.66420361012185936, -6.761305300330741730, 3.999773682894746774 ) ) ;
#1878=CARTESIAN_POINT ( 'NONE',  ( 41.34499449510862235, -4.297820755683611438, 1.873789611272388189 ) ) ;
#1887=CARTESIAN_POINT ( 'NONE',  ( 23.90742340929273624, -3.204431202270332513, -2.713652344655542503 ) ) ;
#1893=CARTESIAN_POINT ( 'NONE',  ( 28.69353846085885706, -5.618139531230570860, -3.997238537426948568 ) ) ;
#1898=CARTESIAN_POINT ( 'NONE',  ( 19.10390797508228999, -2.015740111943971957, 1.010822989962091301 ) ) ;
#1934=B_SPLINE_CURVE_WITH_KNOTS ( 'NONE', 3,
 ( #23308, #18286, #12930, #12754, #18459, #10932, #13251, #20794, #28498, #22959 ),
 .UNSPECIFIED., .F., .F.,
 ( 4, 3, 3, 4 ),
 ( 0.000000000000000000, 0.0005351973326734103635, 0.001070394665346820727, 0.002130599681840938692 ),
 .UNSPECIFIED. ) ;
#1936=CARTESIAN_POINT ( 'NONE',  ( 29.31981545345093920, -4.303267367677382715, -2.184956339556331173 ) ) ;
#1951=CARTESIAN_POINT ( 'NONE',  ( 29.25343337322282622, -7.426690278353109242, 4.522129901861163148 ) ) ;
#1968=CARTESIAN_POINT ( 'NONE',  ( 85.00835009346432969, -4.756612885510127953, -4.312042181587000478 ) ) ;
#1978=CARTESIAN_POINT ( 'NONE',  ( 85.08949032934708612, -1.315411135598755221, 0.07017451552781951707 ) ) ;
#1991=CARTESIAN_POINT ( 'NONE',  ( 69.29300722455955963, -6.224615717686389438, -5.695980980372493008 ) ) ;
#1999=CARTESIAN_POINT ( 'NONE',  ( 69.06996892930607146, -6.106740143811350663, 4.008637876655180676 ) ) ;
#2028=CARTESIAN_POINT ( 'NONE',  ( 23.84149738812723740, -4.050734785762162282, 2.184956778860680959 ) ) ;
#2040=CARTESIAN_POINT ( 'NONE',  ( 28.69343354123121514, -5.622193070524895475, -4.003574682336918933 ) ) ;
#2093=CARTESIAN_POINT ( 'NONE',  ( 29.11693253002209403, -8.303828435806185126, -0.02339150517595086839 ) ) ;
#2094=CARTESIAN_POINT ( 'NONE',  ( 23.84714171513466141, -3.444070612163574463, -0.07017451552781628354 ) ) ;
#2104=DIRECTION ( 'NONE',  ( 1.000000000000000000, 0.000000000000000000, 0.000000000000000000 ) ) ;
#2106=B_SPLINE_CURVE_WITH_KNOTS ( 'NONE', 3,
 ( #33010, #30505, #2586, #21131, #24099, #554, #23936, #25983, #21277, #8741 ),
 .UNSPECIFIED., .F., .F.,
 ( 4, 3, 3, 4 ),
 ( 0.000000000000000000, 0.0005352520061641840221, 0.001070504012328368695, 0.002130599681840939126 ),
 .UNSPECIFIED. ) ;
#2141=CARTESIAN_POINT ( 'NONE',  ( 29.27825211595695976, -6.695835137279975591, -5.695980980372493008 ) ) ;
#2149=CARTESIAN_POINT ( 'NONE',  ( 18.75975746536424538, -5.862652109951548951, 4.018750267660987419 ) ) ;
#2168=ORIENTED_EDGE ( 'NONE', *, *, #24650, .F. ) ;
#2183=CARTESIAN_POINT ( 'NONE',  ( 84.86147853070771419, -2.382337935103847393, 0.8105612886933132311 ) ) ;
#2195=CARTESIAN_POINT ( 'NONE',  ( 102.3445399775881555, -2.862965201256810310, -4.006107067522454379 ) ) ;
#2205=VERTEX_POINT ( 'NONE', #8646 ) ;
#2209=EDGE_CURVE ( 'NONE', #25625, #22238, #27212, .T. ) ;
#2269=CARTESIAN_POINT ( 'NONE',  ( 35.16139127360178662, -8.400504373793673096, -0.07017451552783579571 ) ) ;
#2272=CARTESIAN_POINT ( 'NONE',  ( 85.33608266635168604, -5.304379108986591262, 5.695980980372492120 ) ) ;
#2312=CARTESIAN_POINT ( 'NONE',  ( 101.7092342197782671, -2.711528754415359455, -3.693496777363507899 ) ) ;
#2335=ORIENTED_EDGE ( 'NONE', *, *, #14787, .F. ) ;
#2339=CARTESIAN_POINT ( 'NONE',  ( 54.97704564079767664, -6.500107750844804855, 4.003574679610500731 ) ) ;
#2370=CARTESIAN_POINT ( 'NONE',  ( 84.89587746248274414, -2.934653466126000421, 2.184955971586097778 ) ) ;
#2375=CARTESIAN_POINT ( 'NONE',  ( 69.32965659118902124, -6.955028994486257332, 4.522129901861162260 ) ) ;
#2385=CARTESIAN_POINT ( 'NONE',  ( 54.94565165835368958, -5.365794815109278026, -4.003574679618516541 ) ) ;
#2391=CARTESIAN_POINT ( 'NONE',  ( 69.38611993481310947, -8.080330187051609769, -2.713652344655542059 ) ) ;
#2406=CARTESIAN_POINT ( 'NONE',  ( 18.93617721851659041, -3.890633339435721982, 4.522129901861162260 ) ) ;
#2434=ORIENTED_EDGE ( 'NONE', *, *, #7297, .F. ) ;
#2446=CARTESIAN_POINT ( 'NONE',  ( 54.77277180716814087, -8.244003004416214253, -0.07017451552783579571 ) ) ;
#2448=CARTESIAN_POINT ( 'NONE',  ( 47.68482864957696421, -3.825617316378856714, 0.02339150516272765420 ) ) ;
#2502=CARTESIAN_POINT ( 'NONE',  ( 85.03368400521037529, -5.169987188093748465, 4.043899880995859952 ) ) ;
#2525=CARTESIAN_POINT ( 'NONE',  ( 54.93487251132799543, -4.984033517862624052, 3.390608480937900460 ) ) ;
#2539=CARTESIAN_POINT ( 'NONE',  ( 54.94569726418254163, -5.367442601113908474, -4.006107073548754727 ) ) ;
#2554=CARTESIAN_POINT ( 'NONE',  ( 102.6609843814833027, -1.982062027707615970, 4.522129901861162260 ) ) ;
#2586=CARTESIAN_POINT ( 'NONE',  ( 18.87735372170065418, -4.548161977172891390, 3.690548956284755544 ) ) ;
#2590=CARTESIAN_POINT ( 'NONE',  ( 41.45135008765516460, -9.497951668093163491, 0.07017451552781736601 ) ) ;
#2598=CARTESIAN_POINT ( 'NONE',  ( 41.19430503359171780, -3.886431767412232841, -0.02339150518254430253 ) ) ;
#2621=VERTEX_POINT ( 'NONE', #26360 ) ;
#2622=CARTESIAN_POINT ( 'NONE',  ( 41.45135008765516460, -9.497951668093168820, 1.010822989962089746 ) ) ;
#2631=CARTESIAN_POINT ( 'NONE',  ( 102.9885081044300676, -6.698322160490901567, -0.07017451552783579571 ) ) ;
#2651=CARTESIAN_POINT ( 'NONE',  ( 40.88348196906002130, -6.802589077584822341, 4.112224033454269900 ) ) ;
#2682=CARTESIAN_POINT ( 'NONE',  ( 19.01480233880980819, -3.011762293215293429, 0.07017451552782509594 ) ) ;
#2689=EDGE_CURVE ( 'NONE', #3757, #13458, #26878, .T. ) ;
#2690=FACE_OUTER_BOUND ( 'NONE', #26329, .T. ) ;
#2696=CARTESIAN_POINT ( 'NONE',  ( 28.69334747239712513, -5.625518540330015860, -4.008637382338393174 ) ) ;
#2731=EDGE_CURVE ( 'NONE', #13458, #28727, #30102, .T. ) ;
#2735=CARTESIAN_POINT ( 'NONE',  ( 18.51491971917340607, -8.599446730134173933, 0.07017451552781736601 ) ) ;
#2771=CARTESIAN_POINT ( 'NONE',  ( 41.43929652434213295, -5.500819839281759549, 5.695980980372492120 ) ) ;
#2786=CARTESIAN_POINT ( 'NONE',  ( 29.11693253002209403, -8.303828435806185126, 0.07017451552781736601 ) ) ;
#2794=CARTESIAN_POINT ( 'NONE',  ( 19.10390797508229710, -2.015740111943975066, 0.07017451552782062729 ) ) ;
#2797=CARTESIAN_POINT ( 'NONE',  ( 48.09235817783085309, -9.172289267036328297, 1.915219082070893863 ) ) ;
#2841=CARTESIAN_POINT ( 'NONE',  ( 28.66558084216347879, -6.707193022007285954, 4.073741754960026107 ) ) ;
#2865=AXIS2_PLACEMENT_3D ( 'NONE', #14796, #7619, #2104 ) ;
#2880=CARTESIAN_POINT ( 'NONE',  ( 41.35640441664088485, -8.240600375908496034, 1.529340244835370344 ) ) ;
#2893=CARTESIAN_POINT ( 'NONE',  ( 40.88018956639172075, -6.197502223141884592, -4.312042181581901445 ) ) ;
#2913=VECTOR ( 'NONE', #8060, 1000.000000000000000 ) ;
#2916=EDGE_CURVE ( 'NONE', #6454, #24800, #9340, .T. ) ;
#2918=EDGE_CURVE ( 'NONE', #19057, #19567, #17112, .T. ) ;
#2953=EDGE_CURVE ( 'NONE', #20898, #8159, #202, .T. ) ;
#2957=CARTESIAN_POINT ( 'NONE',  ( 69.10820754288468493, -6.866680491177692858, 2.787783121302774170 ) ) ;
#2962=CARTESIAN_POINT ( 'NONE',  ( 85.25075202023808174, -3.924039320687066290, 5.695980980372492120 ) ) ;
#2993=CARTESIAN_POINT ( 'NONE',  ( 102.5019105821285024, -5.123465467906981985, -2.184956770195078057 ) ) ;
#3007=CARTESIAN_POINT ( 'NONE',  ( 102.2915521900156079, -2.105775436100236764, -2.787782622536843835 ) ) ;
#3012=CARTESIAN_POINT ( 'NONE',  ( 54.97666862915123431, -6.486485553567831630, 4.023790190276410605 ) ) ;
#3024=CARTESIAN_POINT ( 'NONE',  ( 35.27967220683370186, -7.797546999713141247, -2.184956776474153095 ) ) ;
#3033=CARTESIAN_POINT ( 'NONE',  ( 47.95865874067742141, -8.381244160377555374, 0.8105615599371254199 ) ) ;
#3039=CARTESIAN_POINT ( 'NONE',  ( 68.71221462755966058, -6.131929330191479899, -3.993435576825361100 ) ) ;
#3044=CARTESIAN_POINT ( 'NONE',  ( 54.96134875814583154, -5.932951279955770651, -4.312042181584450518 ) ) ;
#3052=CARTESIAN_POINT ( 'NONE',  ( 48.09670199522224721, -9.430894477034977186, -0.07017451552783579571 ) ) ;
#3069=CARTESIAN_POINT ( 'NONE',  ( 18.65791233782715963, -7.001076235476726417, -2.184956778830003277 ) ) ;
#3070=CARTESIAN_POINT ( 'NONE',  ( 28.60502136297058229, -6.760022240753575495, 3.993434336043301336 ) ) ;
#3089=EDGE_CURVE ( 'NONE', #11534, #4598, #24939, .T. ) ;
#3102=CARTESIAN_POINT ( 'NONE',  ( 23.66826818115504238, -7.072331084924259770, 2.787782631216866758 ) ) ;
#3109=CARTESIAN_POINT ( 'NONE',  ( 18.93617721851659041, -3.890633339435721982, 4.522129901861162260 ) ) ;
#3127=CARTESIAN_POINT ( 'NONE',  ( 29.33867311917065379, -3.750126786195063122, -0.8105614676216158498 ) ) ;
#3156=CARTESIAN_POINT ( 'NONE',  ( 40.88367704618155329, -6.838565261165500786, 4.073741263077431896 ) ) ;
#3160=CARTESIAN_POINT ( 'NONE',  ( 18.86054332783663767, -4.736068442360261699, 3.993434336035624366 ) ) ;
#3167=CARTESIAN_POINT ( 'NONE',  ( 41.35325844292879793, -7.141637217093566470, -3.390608916445196908 ) ) ;
#3173=DIRECTION ( 'NONE',  ( 0.000000000000000000, 0.000000000000000000, -1.000000000000000000 ) ) ;
#3178=CARTESIAN_POINT ( 'NONE',  ( 23.61221640758335738, -8.051464822112826880, 0.4367666033528453395 ) ) ;
#3191=CARTESIAN_POINT ( 'NONE',  ( 69.01696383923302847, -5.045148589264282890, -4.093304263523003250 ) ) ;
#3197=CARTESIAN_POINT ( 'NONE',  ( 29.19831543700436427, -9.049787287704358363, -1.915219082070897638 ) ) ;
#3252=FACE_OUTER_BOUND ( 'NONE', #14155, .T. ) ;
#3272=CARTESIAN_POINT ( 'NONE',  ( 29.40513214805973874, -2.959508727827649732, -1.915219082070890755 ) ) ;
#3281=CARTESIAN_POINT ( 'NONE',  ( 68.92628806523653395, -3.240579989648024295, -0.4367667217259110779 ) ) ;
#3294=CARTESIAN_POINT ( 'NONE',  ( 18.65791233782715963, -7.001076235476726417, -2.184956778830003277 ) ) ;
#3303=LINE ( 'NONE', #189, #30538 ) ;
#3319=CARTESIAN_POINT ( 'NONE',  ( 54.94687251578933740, -5.409905656046521294, 4.074610066671965569 ) ) ;
#3334=DIRECTION ( 'NONE',  ( 0.000000000000000000, 0.000000000000000000, 1.000000000000000000 ) ) ;
#3341=ADVANCED_FACE ( 'NONE', ( #27039 ), #24136, .T. ) ;
#3358=CARTESIAN_POINT ( 'NONE',  ( 18.96091535642496240, -3.614110606601101949, 2.184956778829998836 ) ) ;
#3363=DIRECTION ( 'NONE',  ( 0.06927878976713817971, -0.9975973382524637723, 0.000000000000000000 ) ) ;
#3415=CARTESIAN_POINT ( 'NONE',  ( 18.58227844715246135, -7.846511338401735536, -2.713652344655543391 ) ) ;
#3436=CARTESIAN_POINT ( 'NONE',  ( 29.27523314209291527, -3.695744416153337042, 0.07017451552713392660 ) ) ;
#3443=B_SPLINE_CURVE_WITH_KNOTS ( 'NONE', 3,
 ( #20128, #24175, #31880, #26852, #1451, #19155 ),
 .UNSPECIFIED., .F., .F.,
 ( 4, 2, 4 ),
 ( 0.009536920346932386411, 0.5047684601734662158, 1.000000000000000000 ),
 .UNSPECIFIED. ) ;
#3451=ORIENTED_EDGE ( 'NONE', *, *, #11320, .F. ) ;
#3473=CARTESIAN_POINT ( 'NONE',  ( 23.62103335626769152, -7.897478826044957323, -1.169950778993630758 ) ) ;
#3491=CARTESIAN_POINT ( 'NONE',  ( 69.01291188535118692, -4.970031385437840399, -3.993434827419594324 ) ) ;
#3495=CARTESIAN_POINT ( 'NONE',  ( 69.01321520912082974, -4.970018244546921871, 3.993434826753180289 ) ) ;
#3525=CARTESIAN_POINT ( 'NONE',  ( 29.18336473368349715, -8.306880066003914820, 0.4367664981562905946 ) ) ;
#3530=CARTESIAN_POINT ( 'NONE',  ( 85.03579748202663779, -5.204477564423076963, 3.993433529915562108 ) ) ;
#3553=CARTESIAN_POINT ( 'NONE',  ( 101.8667766209797634, -4.980100140098701722, -2.484925282884729913 ) ) ;
#3610=CARTESIAN_POINT ( 'NONE',  ( 54.90427307175370686, -3.885678510653091777, -1.529339875078414179 ) ) ;
#3618=CARTESIAN_POINT ( 'NONE',  ( 47.95865874067742851, -8.381244160376988717, -0.8105615599411728489 ) ) ;
#3642=CARTESIAN_POINT ( 'NONE',  ( 18.84046687333678705, -4.960482910705372284, 4.215290389460252918 ) ) ;
#3654=CARTESIAN_POINT ( 'NONE',  ( 18.60865963056891559, -7.551622653696671073, 0.8125824237645643544 ) ) ;
#3674=CARTESIAN_POINT ( 'NONE',  ( 28.66410178491977945, -6.765307663810779637, 3.993434336021463693 ) ) ;
#3698=CARTESIAN_POINT ( 'NONE',  ( 101.8797206818349821, -5.166491396337139719, -2.184956718990371805 ) ) ;
#3701=B_SPLINE_CURVE_WITH_KNOTS ( 'NONE', 3,
 ( #25976, #31169, #8069, #7580, #28293, #25626, #15265, #12916 ),
 .UNSPECIFIED., .F., .F.,
 ( 4, 2, 2, 4 ),
 ( 0.000000000000000000, 0.5000000000000000000, 0.7500000000000000000, 1.000000000000000000 ),
 .UNSPECIFIED. ) ;
#3716=CARTESIAN_POINT ( 'NONE',  ( 69.01329431673670456, -4.971603792614007311, -3.995971199217486447 ) ) ;
#3751=CARTESIAN_POINT ( 'NONE',  ( 23.90742340928847653, -3.204431202321702088, -2.713652344655540727 ) ) ;
#3757=VERTEX_POINT ( 'NONE', #17951 ) ;
#3761=CARTESIAN_POINT ( 'NONE',  ( 47.88260332741770497, -3.822977517009024329, -0.4367665431853247071 ) ) ;
#3770=CARTESIAN_POINT ( 'NONE',  ( 69.15727116336866231, -7.845927800133502217, -0.4367667211789117987 ) ) ;
#3796=CARTESIAN_POINT ( 'NONE',  ( 28.68519643166255761, -5.941144522469937961, 4.275175838854671007 ) ) ;
#3799=CARTESIAN_POINT ( 'NONE',  ( 19.03654924710325602, -2.768675503676416572, 2.713652344655542503 ) ) ;
#3800=CARTESIAN_POINT ( 'NONE',  ( 102.3664313161150972, -3.178976151073279244, -4.275175836085992387 ) ) ;
#3892=CARTESIAN_POINT ( 'NONE',  ( 84.96582260358789540, -4.062957753267931515, -3.999772873837519338 ) ) ;
#3903=CARTESIAN_POINT ( 'NONE',  ( 101.8016823592329274, -4.042758964359259188, -3.993434276136486716 ) ) ;
#3938=ORIENTED_EDGE ( 'NONE', *, *, #922, .F. ) ;
#3949=CARTESIAN_POINT ( 'NONE',  ( 101.8933637717135667, -5.362948496614666993, 1.868788700022515181 ) ) ;
#3953=CARTESIAN_POINT ( 'NONE',  ( 47.95950916398560082, -8.432626694227655761, -0.07017451552783438018 ) ) ;
#3960=DIRECTION ( 'NONE',  ( 0.06927878976713691683, -0.9975973382524638833, 0.000000000000000000 ) ) ;
#3979=CARTESIAN_POINT ( 'NONE',  ( 40.88018956635887946, -6.197502223173953162, 4.312042181588143563 ) ) ;
#3983=CARTESIAN_POINT ( 'NONE',  ( 102.3530718240336057, -2.986125964273158129, -4.150065902008639895 ) ) ;
#3995=CARTESIAN_POINT ( 'NONE',  ( 19.10390797508231131, -2.015740111943978619, 0.07017451552781951707 ) ) ;
#4006=CARTESIAN_POINT ( 'NONE',  ( 48.02957825751260401, -5.434743900603434597, -5.695980980372493008 ) ) ;
#4020=ORIENTED_EDGE ( 'NONE', *, *, #6524, .F. ) ;
#4042=CARTESIAN_POINT ( 'NONE',  ( 18.99190826319515324, -3.267672110760487136, 1.529339877371808987 ) ) ;
#4054=EDGE_LOOP ( 'NONE', ( #29370, #26954, #19470, #20740 ) ) ;
#4057=CARTESIAN_POINT ( 'NONE',  ( 54.94550075121934185, -5.360342395864071463, -3.995006645025575232 ) ) ;
#4078=ORIENTED_EDGE ( 'NONE', *, *, #29184, .T. ) ;
#4100=CARTESIAN_POINT ( 'NONE',  ( 41.34499449509760893, -4.297820755681335925, -1.873789611272560718 ) ) ;
#4110=DIRECTION ( 'NONE',  ( -0.08910563629484158366, -0.9960221812693186294, 0.000000000000000000 ) ) ;
#4124=VERTEX_POINT ( 'NONE', #30288 ) ;
#4142=CARTESIAN_POINT ( 'NONE',  ( 69.09268213438591033, -2.232183665269761086, -0.07017451552781628354 ) ) ;
#4150=ORIENTED_EDGE ( 'NONE', *, *, #30056, .T. ) ;
#4164=CARTESIAN_POINT ( 'NONE',  ( 69.07033661638675426, -6.114099455435076713, 3.997239029219557871 ) ) ;
#4180=ORIENTED_EDGE ( 'NONE', *, *, #15880, .T. ) ;
#4190=CARTESIAN_POINT ( 'NONE',  ( 35.33570769238654918, -4.203675997508045548, 1.873789188777248871 ) ) ;
#4193=CARTESIAN_POINT ( 'NONE',  ( 29.18953645666586638, -9.308308156628569918, -0.07017451552783579571 ) ) ;
#4201=CARTESIAN_POINT ( 'NONE',  ( 54.94547365672024597, -5.359363431720396420, -3.993434333307572359 ) ) ;
#4206=CARTESIAN_POINT ( 'NONE',  ( 41.44907012427937332, -8.741883605783066002, -2.713652344655542059 ) ) ;
#4260=EDGE_CURVE ( 'NONE', #20898, #15360, #9636, .T. ) ;
#4261=EDGE_CURVE ( 'NONE', #14918, #19163, #27480, .T. ) ;
#4268=ORIENTED_EDGE ( 'NONE', *, *, #29875, .T. ) ;
#4284=CARTESIAN_POINT ( 'NONE',  ( 18.65791233782715963, -7.001076235476726417, -2.184956778830003277 ) ) ;
#4287=CARTESIAN_POINT ( 'NONE',  ( 102.4232908028701985, -3.999773562678796690, -3.993434327364950853 ) ) ;
#4293=EDGE_CURVE ( 'NONE', #1346, #29154, #16686, .T. ) ;
#4295=CARTESIAN_POINT ( 'NONE',  ( 18.92729423629925378, -3.989927253179415878, -2.790733528450975331 ) ) ;
#4301=CARTESIAN_POINT ( 'NONE',  ( 47.98568197278775216, -2.821418575600922019, 0.07017451552781951707 ) ) ;
#4323=CARTESIAN_POINT ( 'NONE',  ( 41.35597062189852835, -8.086568374297849360, 1.873789609323120331 ) ) ;
#4328=ADVANCED_FACE ( 'NONE', ( #2690 ), #31090, .T. ) ;
#4331=CARTESIAN_POINT ( 'NONE',  ( 18.75849706888935131, -5.876740812950394854, 3.997238537398870584 ) ) ;
#4366=CARTESIAN_POINT ( 'NONE',  ( 54.91389575943538404, -4.233367447935240335, 2.184956776131665279 ) ) ;
#4369=CARTESIAN_POINT ( 'NONE',  ( 101.6570814670602374, -1.960542089248300535, 2.484897212538878186 ) ) ;
#4373=CARTESIAN_POINT ( 'NONE',  ( 29.35001421184127324, -4.582605737176272953, -4.522129901861162260 ) ) ;
#4382=CARTESIAN_POINT ( 'NONE',  ( 69.01321520914181917, -4.970018244500666427, -3.993434826699699514 ) ) ;
#4389=CARTESIAN_POINT ( 'NONE',  ( 29.38825086720287771, -3.456623792451290811, 2.713652344655541615 ) ) ;
#4439=CARTESIAN_POINT ( 'NONE',  ( 35.33811999952403227, -4.049688432971476182, -1.529339875353190825 ) ) ;
#4443=CARTESIAN_POINT ( 'NONE',  ( 18.51491971917340607, -8.599446730134173933, 0.07017451552781736601 ) ) ;
#4454=CARTESIAN_POINT ( 'NONE',  ( 41.19430503359171070, -3.886431767412232396, 0.02339150516273359043 ) ) ;
#4455=ADVANCED_FACE ( 'NONE', ( #1496 ), #6252, .F. ) ;
#4479=CARTESIAN_POINT ( 'NONE',  ( 18.77836082091640080, -5.654703931375024695, -4.215290389458773213 ) ) ;
#4490=CARTESIAN_POINT ( 'NONE',  ( 69.09268213438591033, -2.232183665269761086, 0.07017451552781951707 ) ) ;
#4496=DIRECTION ( 'NONE',  ( -0.08910563629484094528, -0.9960221812693187404, 0.000000000000000000 ) ) ;
#4514=CARTESIAN_POINT ( 'NONE',  ( 54.97700003622870213, -6.498459964805339162, 4.006107073540763786 ) ) ;
#4526=CIRCLE ( 'NONE', #9860, 4.999999999999999112 ) ;
#4533=VERTEX_POINT ( 'NONE', #4284 ) ;
#4542=CARTESIAN_POINT ( 'NONE',  ( 54.90427307174406479, -3.885678510653658879, 1.529339875079268829 ) ) ;
#4543=CARTESIAN_POINT ( 'NONE',  ( 85.45070076415389337, -7.158483446636730640, 2.713652344655544724 ) ) ;
#4556=CARTESIAN_POINT ( 'NONE',  ( 54.94583599702954757, -5.372455163404658229, -4.013697991747248395 ) ) ;
#4560=CARTESIAN_POINT ( 'NONE',  ( 47.99837860531645362, -3.577301031424839906, 2.713652344655541615 ) ) ;
#4587=LINE ( 'NONE', #17441, #7019 ) ;
#4598=VERTEX_POINT ( 'NONE', #25670 ) ;
#4607=DIRECTION ( 'NONE',  ( -0.9960221812693186294, 0.08910563629484180570, 0.000000000000000000 ) ) ;
#4609=CARTESIAN_POINT ( 'NONE',  ( 23.84714171513466141, -3.444070612163573575, 0.02339150516273077324 ) ) ;
#4643=CARTESIAN_POINT ( 'NONE',  ( 18.80941384712784981, -5.307593421039076276, -3.636029349014984202 ) ) ;
#4650=ORIENTED_EDGE ( 'NONE', *, *, #18095, .T. ) ;
#4655=CARTESIAN_POINT ( 'NONE',  ( 41.44907012423725234, -8.741883605788331124, -2.713652344655543391 ) ) ;
#4663=CARTESIAN_POINT ( 'NONE',  ( 18.75945136020123982, -5.866073751327065544, 4.013697994447678496 ) ) ;
#4665=B_SPLINE_CURVE_WITH_KNOTS ( 'NONE', 3,
 ( #30234, #27379, #12309, #30069, #25189, #7306, #17496, #12796, #2312, #7816 ),
 .UNSPECIFIED., .F., .F.,
 ( 4, 3, 3, 4 ),
 ( 0.000000000000000000, 0.0005352572989639532318, 0.001070514597927906897, 0.002130599830189221569 ),
 .UNSPECIFIED. ) ;
#4695=CARTESIAN_POINT ( 'NONE',  ( 29.33867311914967146, -3.750126786196623652, 0.8105614676246016836 ) ) ;
#4710=CARTESIAN_POINT ( 'NONE',  ( 69.01386799616022927, -4.983101923413928880, -4.013698489648152901 ) ) ;
#4714=CARTESIAN_POINT ( 'NONE',  ( 29.21519671781910077, -8.552672223075463265, -2.713652344655542059 ) ) ;
#4765=CARTESIAN_POINT ( 'NONE',  ( 54.64624227588102201, -3.635739347938792054, -0.07017451552781628354 ) ) ;
#4769=ORIENTED_EDGE ( 'NONE', *, *, #20957, .F. ) ;
#4786=CARTESIAN_POINT ( 'NONE',  ( 69.06793210257949056, -6.065973107585926449, -4.074610585182336209 ) ) ;
#4818=CARTESIAN_POINT ( 'NONE',  ( 85.03555310018248292, -5.200489395553704597, 3.999772873871539680 ) ) ;
#4821=CARTESIAN_POINT ( 'NONE',  ( 18.97846294920850241, -3.417963736839119360, -1.868788737059456029 ) ) ;
#4853=CARTESIAN_POINT ( 'NONE',  ( 18.58227844715246135, -7.846511338401735536, 2.713652344655544724 ) ) ;
#4864=CARTESIAN_POINT ( 'NONE',  ( 84.96769306194079263, -4.093459866477664910, -4.043899880962059434 ) ) ;
#4891=EDGE_CURVE ( 'NONE', #11796, #22238, #10772, .T. ) ;
#4918=EDGE_LOOP ( 'NONE', ( #25985, #9610, #14730, #18902 ) ) ;
#4930=CARTESIAN_POINT ( 'NONE',  ( 41.43709133142961321, -4.769546740945156849, -4.522129901861162260 ) ) ;
#4943=CARTESIAN_POINT ( 'NONE',  ( 68.56906952848913761, -3.255983411058661847, 0.07017451550800900273 ) ) ;
#4957=VECTOR ( 'NONE', #3173, 1000.000000000000000 ) ;
#4960=CARTESIAN_POINT ( 'NONE',  ( 101.8016823592329274, -4.042758964359259188, -3.993434276136486716 ) ) ;
#4962=CARTESIAN_POINT ( 'NONE',  ( 68.79832465278998654, -7.861404707920828905, 0.07017451552781736601 ) ) ;
#4983=ADVANCED_FACE ( 'NONE', ( #13577 ), #15853, .T. ) ;
#4996=CARTESIAN_POINT ( 'NONE',  ( 69.38611993481310947, -8.080330187063884395, -2.713652344655543391 ) ) ;
#5009=CARTESIAN_POINT ( 'NONE',  ( 28.66858063836256676, -6.589466490307128943, 4.185347664752067764 ) ) ;
#5051=CARTESIAN_POINT ( 'NONE',  ( 18.85937633404960678, -4.749113090755953337, -4.013697994455524665 ) ) ;
#5102=CARTESIAN_POINT ( 'NONE',  ( 18.93617721851659041, -3.890633339435721982, -4.522129901861162260 ) ) ;
#5110=CARTESIAN_POINT ( 'NONE',  ( 84.37491783462850492, -2.359815117480457136, -0.02339150518254430253 ) ) ;
#5112=CARTESIAN_POINT ( 'NONE',  ( 69.29300722455955963, -6.224615717686389438, 5.695980980372492120 ) ) ;
#5135=CARTESIAN_POINT ( 'NONE',  ( 23.57316428367447614, -9.051964865574914754, 1.010822989962089746 ) ) ;
#5157=CARTESIAN_POINT ( 'NONE',  ( 18.58227844715246135, -7.846511338401735536, -2.713652344655542947 ) ) ;
#5164=CARTESIAN_POINT ( 'NONE',  ( 40.88358382947309622, -6.821371083843753347, 4.093303308732203938 ) ) ;
#5169=ORIENTED_EDGE ( 'NONE', *, *, #32303, .F. ) ;
#5197=CARTESIAN_POINT ( 'NONE',  ( 84.55169161418007207, -5.233307109646406552, -3.993432236203768415 ) ) ;
#5202=CARTESIAN_POINT ( 'NONE',  ( 69.01353589305286107, -4.976445672242260976, -4.003575175710716749 ) ) ;
#5217=EDGE_CURVE ( 'NONE', #24285, #20812, #19711, .T. ) ;
#5235=CARTESIAN_POINT ( 'NONE',  ( 41.45135008765516460, -9.497951668093163491, 0.07017451552781736601 ) ) ;
#5250=ORIENTED_EDGE ( 'NONE', *, *, #12875, .T. ) ;
#5264=CARTESIAN_POINT ( 'NONE',  ( 29.11693253002209403, -8.303828435806185126, -0.07017451552783579571 ) ) ;
#5276=CARTESIAN_POINT ( 'NONE',  ( 18.78902641282511254, -5.535484019313972048, -4.282223223018096547 ) ) ;
#5298=FACE_OUTER_BOUND ( 'NONE', #17246, .T. ) ;
#5303=CARTESIAN_POINT ( 'NONE',  ( 23.58234648083524831, -8.048792613698571685, 0.07017451552781737989 ) ) ;
#5316=( BOUNDED_SURFACE ( )  B_SPLINE_SURFACE ( 3, 3, ( 
 ( #18147, #15958, #10472, #300, #30550, #23667, #28038, #10794 ),
 ( #18001, #28346, #8124, #20337, #2622, #10306, #5135, #13138 ),
 ( #5462, #443, #5635, #2797, #15310, #23191, #12977, #15655 ),
 ( #20525, #15814, #13284, #25866, #25514, #28187, #22996, #12787 ) ),
 .UNSPECIFIED., .F., .F., .F. ) 
 B_SPLINE_SURFACE_WITH_KNOTS ( ( 4, 4 ),
 ( 4, 2, 2, 4 ),
 ( 0.000000000000000000, 1.000000000000000000 ),
 ( 0.000000000000000000, 0.5000000000000000000, 0.7500000000000000000, 1.000000000000000000 ),
 .UNSPECIFIED. ) 
 GEOMETRIC_REPRESENTATION_ITEM ( )  RATIONAL_B_SPLINE_SURFACE ( (
 ( 1.000000000000000000, 1.000000000000000000, 1.000000000000000000, 1.000000000000000000, 1.000000000000000000, 1.000000000000000000, 1.000000000000000000, 1.000000000000000000),
 ( 0.9743068154145673176, 0.9743068154145673176, 0.9743068154145673176, 0.9743068154145673176, 0.9743068154145673176, 0.9743068154145673176, 0.9743068154145673176, 0.9743068154145673176),
 ( 0.9743068154145673176, 0.9743068154145673176, 0.9743068154145673176, 0.9743068154145673176, 0.9743068154145673176, 0.9743068154145673176, 0.9743068154145673176, 0.9743068154145673176),
 ( 1.000000000000000000, 1.000000000000000000, 1.000000000000000000, 1.000000000000000000, 1.000000000000000000, 1.000000000000000000, 1.000000000000000000, 1.000000000000000000) ) ) 
 REPRESENTATION_ITEM ( '' )  SURFACE ( )  );
#5320=CARTESIAN_POINT ( 'NONE',  ( 69.06670222590935282, -6.041353941581823150, 4.093304263520331610 ) ) ;
#5337=AXIS2_PLACEMENT_3D ( 'NONE', #275, #4607, #25148 ) ;
#5349=CARTESIAN_POINT ( 'NONE',  ( 47.88260332740731684, -3.822977517009183757, 0.07017451552782355551 ) ) ;
#5350=CARTESIAN_POINT ( 'NONE',  ( 47.95950916398559372, -8.432626694227655761, 0.07017451552782036361 ) ) ;
#5360=ORIENTED_EDGE ( 'NONE', *, *, #2918, .F. ) ;
#5363=CARTESIAN_POINT ( 'NONE',  ( 40.87814480304709264, -5.823931514470607418, -4.093303308743350577 ) ) ;
#5369=CARTESIAN_POINT ( 'NONE',  ( 29.18953645666586638, -9.308308156628569918, -0.07017451552783579571 ) ) ;
#5379=ORIENTED_EDGE ( 'NONE', *, *, #1479, .F. ) ;
#5399=CARTESIAN_POINT ( 'NONE',  ( 69.42401195566040428, -8.835509274236315491, 0.07017451552781736601 ) ) ;
#5417=ORIENTED_EDGE ( 'NONE', *, *, #8565, .T. ) ;
#5435=CARTESIAN_POINT ( 'NONE',  ( 102.5829460782277351, -0.8583298743146007270, 2.713652344655542503 ) ) ;
#5439=AXIS2_PLACEMENT_3D ( 'NONE', #394, #10571, #28478 ) ;
#5448=CARTESIAN_POINT ( 'NONE',  ( 85.08949032934707191, -1.315411135598755665, -0.07017451552781585333 ) ) ;
#5462=CARTESIAN_POINT ( 'NONE',  ( 102.9705908278152293, -6.440317834495091098, 1.915219082070893863 ) ) ;
#5502=CARTESIAN_POINT ( 'NONE',  ( 85.02506012475970465, -5.029259295701730359, 4.185347070121443913 ) ) ;
#5529=CARTESIAN_POINT ( 'NONE',  ( 19.10390797508231131, -2.015740111943978619, 0.07017451552781736601 ) ) ;
#5537=CARTESIAN_POINT ( 'NONE',  ( 47.95695783165739101, -8.278479088713725176, 1.169950612927739941 ) ) ;
#5549=CARTESIAN_POINT ( 'NONE',  ( 69.01610696340840434, -5.027975611445920201, -4.073742241459672897 ) ) ;
#5590=EDGE_LOOP ( 'NONE', ( #2168, #22912, #27092, #22642 ) ) ;
#5626=CARTESIAN_POINT ( 'NONE',  ( 69.09268213438589612, -2.232183665269760198, -0.07017451552781585333 ) ) ;
#5635=CARTESIAN_POINT ( 'NONE',  ( 69.41104820195521086, -8.577144703210713317, 1.915219082070893863 ) ) ;
#5636=CARTESIAN_POINT ( 'NONE',  ( 102.5829460782277351, -0.8583298743145996168, -2.713652344655541615 ) ) ;
#5661=CARTESIAN_POINT ( 'NONE',  ( 18.76070088238846267, -5.852106601039503531, 4.033870043642440173 ) ) ;
#5686=CARTESIAN_POINT ( 'NONE',  ( 69.15727116336863389, -7.845927800133498664, 0.07017451552781883706 ) ) ;
#5698=CARTESIAN_POINT ( 'NONE',  ( 18.84490165312532284, -4.910910973167541549, -4.185347664746176477 ) ) ;
#5699=VERTEX_POINT ( 'NONE', #5636 ) ;
#5771=CARTESIAN_POINT ( 'NONE',  ( 47.99002579013004777, -3.080023785605704667, -1.915219082070890755 ) ) ;
#5773=CARTESIAN_POINT ( 'NONE',  ( 18.96091535642496240, -3.614110606601104614, -2.184956778830005053 ) ) ;
#5780=CARTESIAN_POINT ( 'NONE',  ( 35.33972979714662443, -3.946928302550533729, -1.169950777403906406 ) ) ;
#5789=CARTESIAN_POINT ( 'NONE',  ( 102.5259499419699125, -5.470455821997665780, -1.529339870041445781 ) ) ;
#5805=MECHANICAL_CONTEXT ( 'NONE', #30225, 'mechanical' ) ;
#5806=CARTESIAN_POINT ( 'NONE',  ( 18.80941384712607700, -5.307593421058961702, 4.312042181584448741 ) ) ;
#5819=CARTESIAN_POINT ( 'NONE',  ( 69.08947486655604564, -6.491576118621911640, -3.390608973715747876 ) ) ;
#5829=CARTESIAN_POINT ( 'NONE',  ( 102.5259499419701683, -5.470455822000431567, 1.529339870033843196 ) ) ;
#5884=CARTESIAN_POINT ( 'NONE',  ( 23.68064580653238949, -7.171681651382474598, -4.522129901861164036 ) ) ;
#5901=CARTESIAN_POINT ( 'NONE',  ( 102.5016417986337274, -5.123484090875773944, 2.184956770154327543 ) ) ;
#5904=CARTESIAN_POINT ( 'NONE',  ( 47.68482864957436362, -3.825617316378707944, 0.07017451552782597024 ) ) ;
#5931=CARTESIAN_POINT ( 'NONE',  ( 47.88260332741746339, -3.822977517009003456, -0.07017451552773958101 ) ) ;
#5970=CARTESIAN_POINT ( 'NONE',  ( 69.01948419709430027, -5.095663605514894279, 4.155405370688038502 ) ) ;
#5988=CARTESIAN_POINT ( 'NONE',  ( 23.64679384717729960, -7.447389048086114016, -2.184956778833867297 ) ) ;
#6008=CARTESIAN_POINT ( 'NONE',  ( 85.13336101766876141, -6.778540831290548851, 1.169950242236417415 ) ) ;
#6021=CARTESIAN_POINT ( 'NONE',  ( 101.7221769401408409, -2.897900707892763439, -3.993434276071010203 ) ) ;
#6037=EDGE_LOOP ( 'NONE', ( #20454, #15710, #10776, #8020 ) ) ;
#6068=EDGE_LOOP ( 'NONE', ( #4180, #5360, #23087, #1763 ) ) ;
#6069=CARTESIAN_POINT ( 'NONE',  ( 102.8580990270160385, -4.820463887425400884, -4.522129901861164036 ) ) ;
#6125=CARTESIAN_POINT ( 'NONE',  ( 18.96044790064761898, -3.619335823787583006, 0.07017451552783579571 ) ) ;
#6148=CARTESIAN_POINT ( 'NONE',  ( 69.05424452631314125, -5.791958783386577103, 4.275175994950480174 ) ) ;
#6180=CARTESIAN_POINT ( 'NONE',  ( 85.03572474060098330, -5.203290465832886902, 3.995335864764280043 ) ) ;
#6199=EDGE_LOOP ( 'NONE', ( #28243, #12681, #8835, #16341, #5417, #5250, #23540, #11167, #29877, #32913, #9541, #13840 ) ) ;
#6210=CARTESIAN_POINT ( 'NONE',  ( 68.79832465278707332, -7.861404707910025991, -0.07017451552783410262 ) ) ;
#6217=CARTESIAN_POINT ( 'NONE',  ( 69.01341435844646810, -4.974009774632454750, -3.999774175339687599 ) ) ;
#6220=CARTESIAN_POINT ( 'NONE',  ( 85.45070076415650817, -7.158483446666923378, -2.713652344655543391 ) ) ;
#6252=B_SPLINE_SURFACE_WITH_KNOTS ( 'NONE', 3, 3, ( 
 ( #31773, #3530, #19204, #26573, #1165, #3674, #11031 ),
 ( #24380, #8992, #19052, #16865, #13531, #8505, #13687 ),
 ( #6496, #8683, #1348, #21385, #11522, #16699, #29592 ),
 ( #23740, #6180, #11674, #24040, #11363, #26909, #11180 ),
 ( #29242, #21567, #26725, #6326, #16364, #16513, #18707 ),
 ( #21870, #9158, #19391, #28911, #855, #31595, #23889 ),
 ( #998, #9339, #4164, #25219, #30255, #17196, #4331 ),
 ( #14329, #32587, #19707, #22552, #7178, #7328, #27711 ),
 ( #27566, #4818, #22725, #20059, #32429, #1847, #24887 ),
 ( #6828, #24533, #17518, #22370, #9491, #12336, #14507 ),
 ( #29906, #9659, #6988, #2339, #12519, #29747, #14999 ),
 ( #32279, #17013, #27405, #4514, #32928, #14689, #27216 ),
 ( #24720, #32768, #1999, #9998, #17372, #20210, #19549 ),
 ( #30406, #12172, #25034, #19884, #7479, #30098, #4663 ),
 ( #12025, #1657, #17683, #14835, #11849, #22058, #2149 ),
 ( #9847, #22220, #15499, #3012, #30589, #15191, #20862 ),
 ( #22873, #26051, #23222, #23523, #12818, #12669, #5661 ),
 ( #23035, #2502, #20374, #10152, #33076, #7672, #30765 ),
 ( #15841, #18028, #17874, #25715, #15342, #13165, #20555 ),
 ( #30912, #638, #28068, #25544, #3156, #2841, #15691 ),
 ( #13313, #155, #5320, #10829, #5164, #25392, #21045 ),
 ( #18178, #10341, #31251, #13013, #2651, #7835, #25899 ),
 ( #10653, #28217, #18369, #20713, #8326, #326, #10501 ),
 ( #7987, #5502, #27893, #28386, #23368, #5009, #472 ),
 ( #31073, #8163, #28567, #6292, #13965, #18521, #28714 ),
 ( #13652, #23856, #6148, #29058, #8812, #1460, #18856 ),
 ( #32045, #31737, #21833, #18669, #16330, #19019, #964 ),
 ( #26683, #6446, #24184, #26539, #29203, #21345, #5806 ),
 ( #26397, #23704, #821, #8639, #3979, #10998, #1312 ),
 ( #21199, #31396, #8472, #31551, #11144, #3796, #11487 ),
 ( #28870, #21681, #16477, #8955, #14150, #31889, #3642 ),
 ( #15988, #26210, #5970, #13796, #24001, #1122, #11317 ),
 ( #11638, #21528, #19165, #3319, #29358, #13491, #16166 ),
 ( #16652, #26862, #3495, #24348, #30217, #14802, #19672 ) ),
 .UNSPECIFIED., .F., .F., .F.,
 ( 4, 3, 3, 3, 3, 3, 3, 3, 3, 3, 3, 4 ),
 ( 4, 3, 4 ),
 ( -2.660026849229521048E-11, 0.001953124973451693261, 0.003906249973503654951, 0.007812499973607578765, 0.01562499997381542639, 0.03124999997423111991, 0.06249999997506251043, 0.1249999999767252845, 0.2499999999800508466, 0.4999999999867019707, 0.7499999999933530948, 1.000000000000004219 ),
 ( 0.003589107913147454587, 0.5017945539568872126, 1.000000000000627054 ),
 .UNSPECIFIED. ) ;
#6260=CARTESIAN_POINT ( 'NONE',  ( 84.85832005755730734, -2.331047133796637638, -0.4367664088709692360 ) ) ;
#6264=CARTESIAN_POINT ( 'NONE',  ( 101.8016823592330127, -4.042758964360499974, 3.993434276137187489 ) ) ;
#6270=CARTESIAN_POINT ( 'NONE',  ( 29.18336473368350426, -8.306880066003914820, -0.4367664981582846662 ) ) ;
#6292=CARTESIAN_POINT ( 'NONE',  ( 54.97099024849422477, -6.281314660089699409, 4.215290387836660990 ) ) ;
#6295=CARTESIAN_POINT ( 'NONE',  ( 54.95170718585931979, -5.584587902124617642, -4.215290387841124975 ) ) ;
#6302=LINE ( 'NONE', #16490, #718 ) ;
#6319=CARTESIAN_POINT ( 'NONE',  ( 55.00869849602042905, -7.632537969515627019, 2.184956776156973035 ) ) ;
#6326=CARTESIAN_POINT ( 'NONE',  ( 54.97717972842301748, -6.504952610483546671, 3.995970705059755268 ) ) ;
#6368=CARTESIAN_POINT ( 'NONE',  ( 40.87773644913306015, -5.749500242219811597, -3.994702139305111199 ) ) ;
#6399=ORIENTED_EDGE ( 'NONE', *, *, #6641, .F. ) ;
#6409=ORIENTED_EDGE ( 'NONE', *, *, #29164, .T. ) ;
#6424=CARTESIAN_POINT ( 'NONE',  ( 55.02542983044660474, -8.237060396196271839, -0.07017451552783633695 ) ) ;
#6443=CIRCLE ( 'NONE', #27293, 4.999999999999999112 ) ;
#6446=CARTESIAN_POINT ( 'NONE',  ( 85.00069437095692138, -4.631723123801140041, 4.312042181584448741 ) ) ;
#6450=CARTESIAN_POINT ( 'NONE',  ( 102.3479907709230616, -2.912778821759231196, -4.073741746338383152 ) ) ;
#6454=VERTEX_POINT ( 'NONE', #17747 ) ;
#6485=CARTESIAN_POINT ( 'NONE',  ( 48.06508596181272708, -7.548662730768715079, -4.522129901861164036 ) ) ;
#6488=CIRCLE ( 'NONE', #28902, 5.000000000000000888 ) ;
#6496=CARTESIAN_POINT ( 'NONE',  ( 102.4232361084521585, -3.998984015183867591, 3.994702627084546709 ) ) ;
#6524=EDGE_CURVE ( 'NONE', #13458, #15872, #17502, .T. ) ;
#6530=B_SPLINE_SURFACE_WITH_KNOTS ( 'NONE', 1, 3, ( 
 ( #30981, #30488, #13235, #18094, #20778, #20467, #7574, #30328 ),
 ( #7757, #17949, #5399, #28136, #5235, #15409, #25620, #2735 ) ),
 .UNSPECIFIED., .F., .F., .F.,
 ( 2, 2 ),
 ( 4, 2, 2, 4 ),
 ( 0.000000000000000000, 1.000000000000000000 ),
 ( 0.000000000000000000, 0.5000000000000000000, 0.7500000000000000000, 1.000000000000000000 ),
 .UNSPECIFIED. ) ;
#6533=CARTESIAN_POINT ( 'NONE',  ( 102.2410647596616116, -1.384237843926831690, 1.529339869964214671 ) ) ;
#6536=CARTESIAN_POINT ( 'NONE',  ( 23.57316428367446193, -9.051964865574909425, -0.07017451552783579571 ) ) ;
#6554=CARTESIAN_POINT ( 'NONE',  ( 54.94556186992998192, -5.362550666240347041, -3.998506278715515005 ) ) ;
#6575=CARTESIAN_POINT ( 'NONE',  ( 102.4237878418650638, -3.999739124950154157, 3.993434327388001748 ) ) ;
#6603=CARTESIAN_POINT ( 'NONE',  ( 47.88941090695973912, -4.233884984401246498, -1.873788949266955273 ) ) ;
#6607=CARTESIAN_POINT ( 'NONE',  ( 101.8797206818347973, -5.166491396334524033, 2.184956718991889257 ) ) ;
#6641=EDGE_CURVE ( 'NONE', #12104, #27444, #26208, .T. ) ;
#6642=CARTESIAN_POINT ( 'NONE',  ( 40.87146290594699849, -4.622005974785199811, 2.184956282062899380 ) ) ;
#6663=ORIENTED_EDGE ( 'NONE', *, *, #12875, .F. ) ;
#6666=CARTESIAN_POINT ( 'NONE',  ( 23.80135741154355244, -5.059951201419124800, -5.695980980372493008 ) ) ;
#6702=CARTESIAN_POINT ( 'NONE',  ( 19.00106589343894825, -3.165308183742224557, 1.169950778989204521 ) ) ;
#6716=CARTESIAN_POINT ( 'NONE',  ( 102.3441463922209920, -2.857283636501866564, -3.997238528716361650 ) ) ;
#6759=CARTESIAN_POINT ( 'NONE',  ( 29.32642088969984329, -4.109531239335385777, -1.873788766282285856 ) ) ;
#6763=CARTESIAN_POINT ( 'NONE',  ( 101.8470492078815255, -4.696030299047205148, 2.942092770106637722 ) ) ;
#6768=CARTESIAN_POINT ( 'NONE',  ( 29.18511942701329787, -8.255514837367675440, -0.8105614686289663862 ) ) ;
#6773=FACE_OUTER_BOUND ( 'NONE', #24834, .T. ) ;
#6794=CARTESIAN_POINT ( 'NONE',  ( 102.4145990881584254, -3.874303363244021359, -4.155404932454223932 ) ) ;
#6824=B_SPLINE_CURVE_WITH_KNOTS ( 'NONE', 3,
 ( #25387, #12327, #17367, #25030, #20204, #10145 ),
 .UNSPECIFIED., .F., .F.,
 ( 4, 2, 4 ),
 ( 0.000000000000000000, 0.001111101129503269625, 0.002222202259006539251 ),
 .UNSPECIFIED. ) ;
#6828=CARTESIAN_POINT ( 'NONE',  ( 102.4229585137539686, -3.994976765484275827, 4.001040673959716187 ) ) ;
#6838=EDGE_LOOP ( 'NONE', ( #15264, #13668, #13693, #6409 ) ) ;
#6853=CARTESIAN_POINT ( 'NONE',  ( 84.89549059757896998, -2.934676561234464742, 2.184955970506698542 ) ) ;
#6866=CARTESIAN_POINT ( 'NONE',  ( 28.69360035299894918, -5.615748452712411520, -3.993434336011448593 ) ) ;
#6870=CARTESIAN_POINT ( 'NONE',  ( 23.93581954902093756, -2.707668749987983237, 1.915219082070892531 ) ) ;
#6885=B_SPLINE_CURVE_WITH_KNOTS ( 'NONE', 3,
 ( #20181, #32903, #30555, #17650, #25519, #14810, #11996, #32556, #14660, #12301 ),
 .UNSPECIFIED., .F., .F.,
 ( 4, 2, 2, 2, 4 ),
 ( 0.000000000000000000, 0.0003410365069723375565, 0.0006820730139446751130, 0.001023109520917012561, 0.001364146027889350226 ),
 .UNSPECIFIED. ) ;
#6888=VERTEX_POINT ( 'NONE', #29630 ) ;
#6912=CARTESIAN_POINT ( 'NONE',  ( 29.33166896510681099, -3.955587949931513858, -1.529339504155426743 ) ) ;
#6929=CARTESIAN_POINT ( 'NONE',  ( 102.8580990270160385, -4.820463887425400884, 4.522129901861163148 ) ) ;
#6950=CARTESIAN_POINT ( 'NONE',  ( 28.66730804928445764, -6.639321322089450916, -4.155404940063424313 ) ) ;
#6977=CARTESIAN_POINT ( 'NONE',  ( 85.25075202023842280, -3.924039320687039645, -5.695980980372493008 ) ) ;
#6988=CARTESIAN_POINT ( 'NONE',  ( 69.07013463293527877, -6.110056736244218634, 4.003575175709323197 ) ) ;
#7019=VECTOR ( 'NONE', #21953, 1000.000000000000114 ) ;
#7040=CARTESIAN_POINT ( 'NONE',  ( 84.96637968728258272, -4.072042218960389093, -4.013697180992776836 ) ) ;
#7115=CARTESIAN_POINT ( 'NONE',  ( 19.01480233880806381, -3.011762293215139330, -0.02339150518254430253 ) ) ;
#7147=VECTOR ( 'NONE', #11438, 1000.000000000000000 ) ;
#7178=CARTESIAN_POINT ( 'NONE',  ( 40.88397423554524579, -6.893404915994589821, 3.998505783848317119 ) ) ;
#7207=CARTESIAN_POINT ( 'NONE',  ( 41.34400607036577924, -3.938209558062384374, 0.8105618912856630276 ) ) ;
#7208=CARTESIAN_POINT ( 'NONE',  ( 29.25343337322282622, -7.426690278353109242, 4.522129901861162260 ) ) ;
#7209=ORIENTED_EDGE ( 'NONE', *, *, #4260, .T. ) ;
#7222=CARTESIAN_POINT ( 'NONE',  ( 18.86011488185538454, -4.740857608533977086, -4.001040682675098381 ) ) ;
#7226=CARTESIAN_POINT ( 'NONE',  ( 47.98568197278774505, -2.821418575600922019, 0.07017451552782173751 ) ) ;
#7289=ORIENTED_EDGE ( 'NONE', *, *, #12921, .F. ) ;
#7293=CARTESIAN_POINT ( 'NONE',  ( 28.67557137524228850, -6.315853537160169395, -4.312042181587000478 ) ) ;
#7297=EDGE_CURVE ( 'NONE', #2621, #21989, #6443, .T. ) ;
#7303=CARTESIAN_POINT ( 'NONE',  ( 18.65791233782715963, -7.001076235476726417, 2.184956778830005497 ) ) ;
#7306=CARTESIAN_POINT ( 'NONE',  ( 101.6768137521178943, -2.244682085303995045, -2.942177603107532402 ) ) ;
#7323=FACE_OUTER_BOUND ( 'NONE', #12666, .T. ) ;
#7328=CARTESIAN_POINT ( 'NONE',  ( 28.66418304177962284, -6.762113744407424853, 3.998506281448072741 ) ) ;
#7368=CARTESIAN_POINT ( 'NONE',  ( 18.85812681186292750, -4.763080241043835095, -4.033870043650071402 ) ) ;
#7374=CARTESIAN_POINT ( 'NONE',  ( 102.5305753040692736, -0.1042037546421159255, 0.07017451552782173751 ) ) ;
#7474=CARTESIAN_POINT ( 'NONE',  ( 85.20563808598696198, -3.194259795296082061, -4.522129901861162260 ) ) ;
#7479=CARTESIAN_POINT ( 'NONE',  ( 40.88392054027885791, -6.883494307245545230, 4.013697493832091290 ) ) ;
#7512=CARTESIAN_POINT ( 'NONE',  ( 84.91897426280726791, -3.309433673477568671, 2.787781823999374797 ) ) ;
#7517=CARTESIAN_POINT ( 'NONE',  ( 85.38119660046028514, -6.034158634444421132, 4.522129901861162260 ) ) ;
#7528=CARTESIAN_POINT ( 'NONE',  ( 102.3444260579792058, -2.861320725351368832, -4.003574673598517819 ) ) ;
#7574=CARTESIAN_POINT ( 'NONE',  ( 23.57316428367674277, -9.051964865549241068, -0.07017451552783579571 ) ) ;
#7580=CARTESIAN_POINT ( 'NONE',  ( 48.08400536259535585, -8.675012021211058411, 2.713652344655544724 ) ) ;
#7606=CARTESIAN_POINT ( 'NONE',  ( 54.64624227588102201, -3.635739347938791610, 0.07017451550800275772 ) ) ;
#7607=CARTESIAN_POINT ( 'NONE',  ( 69.18703749905368738, -4.112663945019823686, 4.522129901861162260 ) ) ;
#7619=DIRECTION ( 'NONE',  ( 0.000000000000000000, 0.000000000000000000, 1.000000000000000000 ) ) ;
#7623=DIRECTION ( 'NONE',  ( 0.06927878976713819359, -0.9975973382524637723, 0.000000000000000000 ) ) ;
#7648=CARTESIAN_POINT ( 'NONE',  ( 23.90742340928847653, -3.204431202321702088, -2.713652344655540727 ) ) ;
#7672=CARTESIAN_POINT ( 'NONE',  ( 28.66498257487024048, -6.730694557050681759, 4.043900693851640860 ) ) ;
#7708=CARTESIAN_POINT ( 'NONE',  ( 69.38611993481310947, -8.080330187051606217, 2.713652344655544724 ) ) ;
#7720=CARTESIAN_POINT ( 'NONE',  ( 18.85746438010532700, -4.770484898610086510, -4.043900693820822845 ) ) ;
#7757=CARTESIAN_POINT ( 'NONE',  ( 102.9885081044300534, -6.698322160490901567, 0.07017451552781736601 ) ) ;
#7768=VERTEX_POINT ( 'NONE', #2406 ) ;
#7781=CARTESIAN_POINT ( 'NONE',  ( 47.75999538435722513, -8.435302152663906483, -0.07017451552783579571 ) ) ;
#7793=CARTESIAN_POINT ( 'NONE',  ( 18.84751037367278315, -4.881750713116288054, -4.171867820445587682 ) ) ;
#7811=EDGE_CURVE ( 'NONE', #19163, #4533, #19051, .T. ) ;
#7816=CARTESIAN_POINT ( 'NONE',  ( 101.7221769401408409, -2.897900707892763439, -3.993434276071010203 ) ) ;
#7828=CARTESIAN_POINT ( 'NONE',  ( 48.08400536259535585, -8.675012021204926427, -2.713652344655543391 ) ) ;
#7835=CARTESIAN_POINT ( 'NONE',  ( 28.66649852640073348, -6.671163739231440459, 4.112224495658902690 ) ) ;
#7852=ORIENTED_EDGE ( 'NONE', *, *, #32172, .F. ) ;
#7857=CARTESIAN_POINT ( 'NONE',  ( 40.87556030649425765, -5.373140178136390332, 3.390607986860986411 ) ) ;
#7863=CARTESIAN_POINT ( 'NONE',  ( 85.12704628545890273, -6.675959057343738401, 1.529339193916483097 ) ) ;
#7866=CARTESIAN_POINT ( 'NONE',  ( 101.8016823592329274, -4.042758964359259188, -3.993434276136486716 ) ) ;
#7869=VERTEX_POINT ( 'NONE', #13375 ) ;
#7871=CARTESIAN_POINT ( 'NONE',  ( 28.69209672924516852, -5.673860896767527251, -4.073741754953343452 ) ) ;
#7888=EDGE_CURVE ( 'NONE', #14918, #1346, #25013, .T. ) ;
#7902=CARTESIAN_POINT ( 'NONE',  ( 68.76824089134748874, -7.257250553475476984, -2.184958019050049050 ) ) ;
#7946=CARTESIAN_POINT ( 'NONE',  ( 47.98568197278774505, -2.821418575600921130, -0.07017451552781585333 ) ) ;
#7956=FACE_OUTER_BOUND ( 'NONE', #16613, .T. ) ;
#7967=EDGE_CURVE ( 'NONE', #23146, #20898, #3303, .T. ) ;
#7980=ADVANCED_FACE ( 'NONE', ( #10023 ), #29218, .F. ) ;
#7987=CARTESIAN_POINT ( 'NONE',  ( 102.4111596038446947, -3.824652436571373659, 4.185347658344710453 ) ) ;
#8013=CARTESIAN_POINT ( 'NONE',  ( 69.15727116336861968, -7.845927800133500440, 0.4367667211769182267 ) ) ;
#8019=CARTESIAN_POINT ( 'NONE',  ( 102.5829460782277351, -0.8583298743146006160, 2.713652344655542503 ) ) ;
#8020=ORIENTED_EDGE ( 'NONE', *, *, #30787, .T. ) ;
#8023=ORIENTED_EDGE ( 'NONE', *, *, #13191, .T. ) ;
#8025=CARTESIAN_POINT ( 'NONE',  ( 85.00069437096559000, -4.631723123766721351, -4.312042181584450518 ) ) ;
#8033=CARTESIAN_POINT ( 'NONE',  ( 69.42401195566041849, -8.835509274224047971, -1.010822989962099960 ) ) ;
#8036=CARTESIAN_POINT ( 'NONE',  ( 18.60402535543785518, -7.603424548862136589, -0.07017451552783579571 ) ) ;
#8060=DIRECTION ( 'NONE',  ( -0.03662738895564519870, 0.5274252892134370096, 0.8488115212910427587 ) ) ;
#8069=CARTESIAN_POINT ( 'NONE',  ( 69.38611993481310947, -8.080330187051606217, 2.713652344655544724 ) ) ;
#8088=CARTESIAN_POINT ( 'NONE',  ( 29.20398424897078726, -7.702373504165580975, 2.184956341284221004 ) ) ;
#8106=CARTESIAN_POINT ( 'NONE',  ( 19.10390797508231131, -2.015740111943978619, -0.07017451552781628354 ) ) ;
#8109=DIRECTION ( 'NONE',  ( -0.9975973382524639943, -0.06927878976713693071, 0.000000000000000000 ) ) ;
#8113=ORIENTED_EDGE ( 'NONE', *, *, #4293, .F. ) ;
#8124=CARTESIAN_POINT ( 'NONE',  ( 69.42401195566040428, -8.835509274224051524, 1.010822989962089746 ) ) ;
#8135=CARTESIAN_POINT ( 'NONE',  ( 29.20401286869407542, -7.702374816469336416, -2.184956341621953513 ) ) ;
#8156=ORIENTED_EDGE ( 'NONE', *, *, #18352, .T. ) ;
#8159=VERTEX_POINT ( 'NONE', #16316 ) ;
#8163=CARTESIAN_POINT ( 'NONE',  ( 85.02201553617686614, -4.979580722693575545, 4.215289907551350801 ) ) ;
#8173=CARTESIAN_POINT ( 'NONE',  ( 18.79914435243739135, -5.422385761091336853, 4.312047644171948413 ) ) ;
#8181=CARTESIAN_POINT ( 'NONE',  ( 18.65791233782715963, -7.001076235476726417, 2.184956778830005497 ) ) ;
#8182=CARTESIAN_POINT ( 'NONE',  ( 47.93698235206657188, -7.077015994068657889, -3.390608234577424884 ) ) ;
#8198=CARTESIAN_POINT ( 'NONE',  ( 41.35669399754907261, -8.343390166155122856, 1.169951067571303849 ) ) ;
#8214=CARTESIAN_POINT ( 'NONE',  ( 69.02196556234740399, -5.145383722448461761, -4.185348026738465954 ) ) ;
#8256=LINE ( 'NONE', #13573, #28306 ) ;
#8273=CARTESIAN_POINT ( 'NONE',  ( 47.93698235206608160, -7.077015994075030569, 3.390608234564004508 ) ) ;
#8280=CARTESIAN_POINT ( 'NONE',  ( 18.51491971917342028, -8.599446730134173933, -0.07017451552783579571 ) ) ;
#8287=CARTESIAN_POINT ( 'NONE',  ( 18.82979855633279698, -5.079733283857774673, -4.282233996325130576 ) ) ;
#8290=CARTESIAN_POINT ( 'NONE',  ( 40.72654494865584240, -4.620392906576441305, -2.184955499788741928 ) ) ;
#8297=CARTESIAN_POINT ( 'NONE',  ( 68.93397511287616908, -3.394585223421259457, -1.169951107274167512 ) ) ;
#8306=CARTESIAN_POINT ( 'NONE',  ( 55.01832146648879274, -7.980226898947390346, -1.529339875107651237 ) ) ;
#8312=CARTESIAN_POINT ( 'NONE',  ( 102.5305753040692736, -0.1042037546421159255, 0.07017451552782062729 ) ) ;
#8320=CARTESIAN_POINT ( 'NONE',  ( 84.89587746248641054, -2.934653466125641152, -2.184955971586068468 ) ) ;
#8325=ADVANCED_FACE ( 'NONE', ( #32532 ), #14686, .T. ) ;
#8326=CARTESIAN_POINT ( 'NONE',  ( 40.88327824823386436, -6.765025065066961218, 4.150065482898403602 ) ) ;
#8331=CARTESIAN_POINT ( 'NONE',  ( 18.81968905113669166, -5.192737262265858078, 4.312036717478699543 ) ) ;
#8338=CARTESIAN_POINT ( 'NONE',  ( 18.60402535544292846, -7.603424548862589560, 0.4426577274541249607 ) ) ;
#8339=CARTESIAN_POINT ( 'NONE',  ( 35.28555349212372505, -7.422113525891726127, -2.787782628876159574 ) ) ;
#8351=CARTESIAN_POINT ( 'NONE',  ( 23.61515526891508188, -8.000136145883233851, 0.8105616806102798888 ) ) ;
#8356=CARTESIAN_POINT ( 'NONE',  ( 29.35001421184127324, -4.582605737176272953, 4.522129901861162260 ) ) ;
#8358=EDGE_CURVE ( 'NONE', #4598, #1159, #13396, .T. ) ;
#8380=CARTESIAN_POINT ( 'NONE',  ( 41.20585001718147566, -8.497180311781161066, 0.07017451552781736601 ) ) ;
#8388=B_SPLINE_SURFACE_WITH_KNOTS ( 'NONE', 1, 3, ( 
 ( #20237, #4543, #7708, #15034, #17903, #14717, #22751, #4853 ),
 ( #20091, #7517, #2375, #25421, #12548, #7208, #22901, #27931 ) ),
 .UNSPECIFIED., .F., .F., .F.,
 ( 2, 2 ),
 ( 4, 2, 2, 4 ),
 ( 0.000000000000000000, 1.000000000000000000 ),
 ( 0.000000000000000000, 0.5000000000000000000, 0.7500000000000000000, 1.000000000000000000 ),
 .UNSPECIFIED. ) ;
#8393=CARTESIAN_POINT ( 'NONE',  ( 29.11693253001929449, -8.303828435806623887, -0.07017451552783451896 ) ) ;
#8405=CARTESIAN_POINT ( 'NONE',  ( 23.61632761762281163, -8.296864917633445913, -2.713652344655543391 ) ) ;
#8454=CARTESIAN_POINT ( 'NONE',  ( 41.35640441665029954, -8.240600375904646668, -1.529340244838580887 ) ) ;
#8467=CARTESIAN_POINT ( 'NONE',  ( 102.3434546416267352, -2.854938759700329953, -3.993434327340286583 ) ) ;
#8472=CARTESIAN_POINT ( 'NONE',  ( 69.02940965802889650, -5.294544073377518423, 4.275175994965093373 ) ) ;
#8477=CARTESIAN_POINT ( 'NONE',  ( 18.82980128142734344, -5.079702822763886516, 4.282223223018092995 ) ) ;
#8499=CARTESIAN_POINT ( 'NONE',  ( 85.14283307489679942, -6.932413485865819069, 0.07017451552782748292 ) ) ;
#8505=CARTESIAN_POINT ( 'NONE',  ( 28.66412654021265283, -6.764326628257229856, 3.995006647739479888 ) ) ;
#8539=VECTOR ( 'NONE', #12570, 1000.000000000000000 ) ;
#8552=CARTESIAN_POINT ( 'NONE',  ( 41.44907012423725234, -8.741883605788331124, -2.713652344655543391 ) ) ;
#8565=EDGE_CURVE ( 'NONE', #11659, #10748, #9013, .T. ) ;
#8599=CARTESIAN_POINT ( 'NONE',  ( 19.00106589343955577, -3.165308183742087778, -1.169950778988538831 ) ) ;
#8630=CARTESIAN_POINT ( 'NONE',  ( 54.91409664899088483, -4.233361888145720009, -2.184956776138697876 ) ) ;
#8639=CARTESIAN_POINT ( 'NONE',  ( 54.95788720335500699, -5.807879973348830660, 4.312042181588143563 ) ) ;
#8646=CARTESIAN_POINT ( 'NONE',  ( 18.60402535544292490, -7.603424548862588672, 0.07017451552782096036 ) ) ;
#8683=CARTESIAN_POINT ( 'NONE',  ( 85.03574907444304642, -5.203687580104308985, 3.994701829074096544 ) ) ;
#8705=B_SPLINE_CURVE_WITH_KNOTS ( 'NONE', 3,
 ( #10675, #15860, #21069, #13818, #23727, #1149, #26709, #16196 ),
 .UNSPECIFIED., .F., .F.,
 ( 4, 2, 2, 4 ),
 ( 0.000000000000000000, 0.5000000000000000000, 0.7500000000000000000, 1.000000000000000000 ),
 .UNSPECIFIED. ) ;
#8741=CARTESIAN_POINT ( 'NONE',  ( 18.96091535642496240, -3.614110606601101949, 2.184956778829998836 ) ) ;
#8753=CARTESIAN_POINT ( 'NONE',  ( 29.22961111230291209, -6.951722887056884126, 3.390608046102742801 ) ) ;
#8790=CARTESIAN_POINT ( 'NONE',  ( 18.60860417056578342, -7.552242585353035054, -0.8105616806102179384 ) ) ;
#8812=CARTESIAN_POINT ( 'NONE',  ( 40.88222826846868685, -6.571667082204984744, 4.275175681024973251 ) ) ;
#8816=CARTESIAN_POINT ( 'NONE',  ( 102.3595522875182837, -3.079674301831176741, -4.215290384261815682 ) ) ;
#8835=ORIENTED_EDGE ( 'NONE', *, *, #12000, .T. ) ;
#8858=CARTESIAN_POINT ( 'NONE',  ( 101.8797206818347973, -5.166491396334524033, 2.184956718991889257 ) ) ;
#8883=CARTESIAN_POINT ( 'NONE',  ( 102.3443137184323177, -2.859699058333353694, -4.001040673967360739 ) ) ;
#8886=CARTESIAN_POINT ( 'NONE',  ( 29.25343337322282622, -7.426690278353109242, -4.522129901861164036 ) ) ;
#8917=B_SPLINE_SURFACE_WITH_KNOTS ( 'NONE', 3, 3, ( 
 ( #27581, #12533, #10014, #20225, #15206, #30118, #17387, #22889, #14850, #11157 ),
 ( #13179, #15708, #5819, #21062, #8182, #3167, #28581, #20726, #31408, #484 ),
 ( #20878, #23538, #978, #28884, #13507, #10849, #8339, #656, #18197, #30926 ),
 ( #10668, #26225, #31093, #21362, #16186, #23720, #3024, #28405, #5988, #13666 ) ),
 .UNSPECIFIED., .F., .F., .F.,
 ( 4, 4 ),
 ( 4, 3, 3, 4 ),
 ( -2.395551311511394542E-13, 1.000000000000001776 ),
 ( 0.003584360682139460345, 0.5017921803410697601, 0.7508960901705348245, 1.000000000000000000 ),
 .UNSPECIFIED. ) ;
#8925=CARTESIAN_POINT ( 'NONE',  ( 23.87614828266676170, -3.446665583135163580, -0.4367666033346507271 ) ) ;
#8940=PLANE ( 'NONE',  #15043 ) ;
#8955=CARTESIAN_POINT ( 'NONE',  ( 54.95170718583340630, -5.584587902149642069, 4.215290387855766596 ) ) ;
#8957=CARTESIAN_POINT ( 'NONE',  ( 69.03558484036936704, -5.418257723488958177, -4.312042181581901445 ) ) ;
#8965=CARTESIAN_POINT ( 'NONE',  ( 18.87719011064256236, -4.549990820396901725, -3.693496858444236697 ) ) ;
#8986=CARTESIAN_POINT ( 'NONE',  ( 69.12709522372956883, -7.241778149835164768, 2.184957268579549083 ) ) ;
#8992=CARTESIAN_POINT ( 'NONE',  ( 85.03573724897340469, -5.203500048815656420, 3.995005841633558319 ) ) ;
#9013=B_SPLINE_CURVE_WITH_KNOTS ( 'NONE', 3,
 ( #22632, #22135, #11933, #27294, #9243, #24951 ),
 .UNSPECIFIED., .F., .F.,
 ( 4, 2, 4 ),
 ( 0.000000000000000000, 0.001111101121386790349, 0.002222202242773580697 ),
 .UNSPECIFIED. ) ;
#9018=CARTESIAN_POINT ( 'NONE',  ( 47.88941090692655678, -4.233884984401186991, 1.873788949266326664 ) ) ;
#9035=CARTESIAN_POINT ( 'NONE',  ( 102.3440361197693278, -2.855691808908399132, -3.994702627092255653 ) ) ;
#9052=CARTESIAN_POINT ( 'NONE',  ( 18.72482702355224404, -6.253104344976480711, 3.390608483624313330 ) ) ;
#9054=CARTESIAN_POINT ( 'NONE',  ( 18.68265047573912341, -6.724553502642427461, -4.522129901861164036 ) ) ;
#9057=DIRECTION ( 'NONE',  ( -0.08910563629484094528, -0.9960221812693187404, 0.000000000000000000 ) ) ;
#9071=ORIENTED_EDGE ( 'NONE', *, *, #2209, .T. ) ;
#9088=CARTESIAN_POINT ( 'NONE',  ( 69.15727116336863389, -7.845927800133500440, -0.07017451552784023661 ) ) ;
#9097=ADVANCED_FACE ( 'NONE', ( #19578 ), #11597, .F. ) ;
#9119=CARTESIAN_POINT ( 'NONE',  ( 28.67878734107521765, -6.190522357037703927, -4.312042181584450518 ) ) ;
#9147=CARTESIAN_POINT ( 'NONE',  ( 102.7116376760606755, -2.711456868667907916, -5.695980980372493008 ) ) ;
#9150=CARTESIAN_POINT ( 'NONE',  ( 69.13676591393961246, -7.435400085124271641, 1.873789664672798727 ) ) ;
#9154=VECTOR ( 'NONE', #18367, 1000.000000000000000 ) ;
#9158=CARTESIAN_POINT ( 'NONE',  ( 85.03567598614395706, -5.202494821364011202, 3.996603857811756200 ) ) ;
#9198=CARTESIAN_POINT ( 'NONE',  ( 68.92628806523022433, -3.240579989648459946, 0.4367667217252174661 ) ) ;
#9205=CARTESIAN_POINT ( 'NONE',  ( 18.93617721851659041, -3.890633339435721982, -4.522129901861162260 ) ) ;
#9214=CARTESIAN_POINT ( 'NONE',  ( 69.01327448684355659, -4.971206343640002245, -3.995337163040377781 ) ) ;
#9234=CARTESIAN_POINT ( 'NONE',  ( 35.29143477761595449, -7.046680052079512535, 3.390608481268459151 ) ) ;
#9243=CARTESIAN_POINT ( 'NONE',  ( 101.6304955275590771, -1.577711174180971065, -1.868788699937914854 ) ) ;
#9302=CARTESIAN_POINT ( 'NONE',  ( 54.96823639741650425, -6.181812932762141166, -4.275175838000669692 ) ) ;
#9309=CARTESIAN_POINT ( 'NONE',  ( 18.91048367622525106, -4.177835576467572309, -3.093621903261461359 ) ) ;
#9316=CARTESIAN_POINT ( 'NONE',  ( 18.96091535642496240, -3.614110606601104614, -2.184956778830005053 ) ) ;
#9330=CARTESIAN_POINT ( 'NONE',  ( 29.35001421184127324, -4.582605737176272953, -4.522129901861162260 ) ) ;
#9334=ORIENTED_EDGE ( 'NONE', *, *, #1479, .T. ) ;
#9339=CARTESIAN_POINT ( 'NONE',  ( 85.03565147854187956, -5.202094871745851279, 3.997237729527196137 ) ) ;
#9340=B_SPLINE_CURVE_WITH_KNOTS ( 'NONE', 3,
 ( #12112, #12261, #15278, #28003, #4930, #15114, #22471, #5102 ),
 .UNSPECIFIED., .F., .F.,
 ( 4, 2, 2, 4 ),
 ( 0.000000000000000000, 0.5000000000000000000, 0.7500000000000000000, 1.000000000000000000 ),
 .UNSPECIFIED. ) ;
#9354=CARTESIAN_POINT ( 'NONE',  ( 102.5305753040692736, -0.1042037546421159255, 0.07017451552782062729 ) ) ;
#9375=CARTESIAN_POINT ( 'NONE',  ( 29.38825086720287771, -3.456623792456554156, -2.713652344655542503 ) ) ;
#9382=CARTESIAN_POINT ( 'NONE',  ( 18.86040190548595419, -4.737649260393223649, -3.995970707755712947 ) ) ;
#9425=CARTESIAN_POINT ( 'NONE',  ( 23.86142584454780646, -3.703306447632950249, -1.529339877351986621 ) ) ;
#9438=CARTESIAN_POINT ( 'NONE',  ( 48.06508596181272708, -7.548662730768715079, 4.522129901861163148 ) ) ;
#9457=CARTESIAN_POINT ( 'NONE',  ( 102.4197966183807296, -3.949332865022705086, -4.074610060379797005 ) ) ;
#9468=PRODUCT_DEFINITION_SHAPE ( 'NONE', 'NONE',  #25774 ) ;
#9491=CARTESIAN_POINT ( 'NONE',  ( 40.88396545762024203, -6.891784699261402913, 4.001040184481850837 ) ) ;
#9518=CARTESIAN_POINT ( 'NONE',  ( 41.34457103395083521, -4.143788916012135282, 1.529340246549222737 ) ) ;
#9534=CARTESIAN_POINT ( 'NONE',  ( 84.96577320347208229, -4.062152178867207475, -3.998505472924086313 ) ) ;
#9539=CARTESIAN_POINT ( 'NONE',  ( 69.09268213438589612, -2.232183665269761086, 0.07017451552782173751 ) ) ;
#9541=ORIENTED_EDGE ( 'NONE', *, *, #2689, .T. ) ;
#9549=EDGE_CURVE ( 'NONE', #7869, #12104, #19162, .T. ) ;
#9578=CARTESIAN_POINT ( 'NONE',  ( 23.84149738812702779, -4.050734785793495440, -2.184956778827896962 ) ) ;
#9594=CARTESIAN_POINT ( 'NONE',  ( 84.37491783462850492, -2.359815117480457136, -0.07017451552781628354 ) ) ;
#9610=ORIENTED_EDGE ( 'NONE', *, *, #27391, .F. ) ;
#9611=CARTESIAN_POINT ( 'NONE',  ( 101.7323099454754072, -3.043813463936519526, -4.171867813696918503 ) ) ;
#9618=CARTESIAN_POINT ( 'NONE',  ( 18.79826502154305601, -5.432214915643744924, -4.312042181587000478 ) ) ;
#9636=CIRCLE ( 'NONE', #24597, 5.000000000000000888 ) ;
#9657=ORIENTED_EDGE ( 'NONE', *, *, #11160, .F. ) ;
#9659=CARTESIAN_POINT ( 'NONE',  ( 85.03540396179919014, -5.198055548956801886, 4.003573871842650789 ) ) ;
#9669=B_SPLINE_CURVE_WITH_KNOTS ( 'NONE', 3,
 ( #413, #31188, #17799, #13254, #26140, #10935 ),
 .UNSPECIFIED., .F., .F.,
 ( 4, 2, 4 ),
 ( 0.000000000000000000, 0.001111101124806939712, 0.002222202249613879424 ),
 .UNSPECIFIED. ) ;
#9697=CARTESIAN_POINT ( 'NONE',  ( 68.92885037296282746, -3.291915072450619650, 0.8105619191588775418 ) ) ;
#9711=CARTESIAN_POINT ( 'NONE',  ( 18.85907022888673978, -4.752534732131552531, -4.018750267668782961 ) ) ;
#9713=ORIENTED_EDGE ( 'NONE', *, *, #2918, .T. ) ;
#9717=CARTESIAN_POINT ( 'NONE',  ( 23.95058674323524528, -2.449331254389988999, 1.010822989962091301 ) ) ;
#9728=CIRCLE ( 'NONE', #20961, 1.676012832569465205 ) ;
#9779=CARTESIAN_POINT ( 'NONE',  ( 54.77277180716814087, -8.244003004416214253, 0.02339150517593243869 ) ) ;
#9806=CARTESIAN_POINT ( 'NONE',  ( 69.05921145840204645, -5.891398902038758045, -4.215290682824791801 ) ) ;
#9825=EDGE_CURVE ( 'NONE', #30917, #6888, #3443, .T. ) ;
#9836=CARTESIAN_POINT ( 'NONE',  ( 85.38119660045754244, -6.034158634414237277, -4.522129901861164036 ) ) ;
#9847=CARTESIAN_POINT ( 'NONE',  ( 102.4219044191236918, -3.979760264920891188, 4.023790184227316047 ) ) ;
#9849=CARTESIAN_POINT ( 'NONE',  ( 19.01016806367753631, -3.063564188380631048, -0.8125824237644804215 ) ) ;
#9860=AXIS2_PLACEMENT_3D ( 'NONE', #6125, #13778, #4110 ) ;
#9886=CARTESIAN_POINT ( 'NONE',  ( 18.85967421310764536, -4.745783400722740630, -4.008637382318521070 ) ) ;
#9913=ORIENTED_EDGE ( 'NONE', *, *, #28715, .F. ) ;
#9939=CARTESIAN_POINT ( 'NONE',  ( 47.75999538435722513, -8.435302152663906483, -0.02339150517595086839 ) ) ;
#9982=CARTESIAN_POINT ( 'NONE',  ( 18.60402535544292490, -7.603424548862588672, 0.07017451552782096036 ) ) ;
#9989=CARTESIAN_POINT ( 'NONE',  ( 85.45070076415650817, -7.158483446666923378, -2.713652344655543391 ) ) ;
#9994=CARTESIAN_POINT ( 'NONE',  ( 85.13613392229150634, -2.069934983084493751, -2.713652344655542503 ) ) ;
#9998=CARTESIAN_POINT ( 'NONE',  ( 54.97695379321813647, -6.496789110673256928, 4.008637379606954987 ) ) ;
#10014=CARTESIAN_POINT ( 'NONE',  ( 69.07074218555992218, -6.116471746196562975, -3.993434826118012371 ) ) ;
#10023=FACE_OUTER_BOUND ( 'NONE', #27685, .T. ) ;
#10026=CARTESIAN_POINT ( 'NONE',  ( 23.87614828266750777, -3.446665583148740719, 0.4367666033252894930 ) ) ;
#10027=CARTESIAN_POINT ( 'NONE',  ( 102.8580990270160385, -4.820463887425400884, 4.522129901861162260 ) ) ;
#10037=CARTESIAN_POINT ( 'NONE',  ( 18.85997003588157384, -4.742476695819044075, -4.003574682316953570 ) ) ;
#10096=CARTESIAN_POINT ( 'NONE',  ( 41.44346753120584026, -6.883984642623635963, 5.695980980372492120 ) ) ;
#10106=ORIENTED_EDGE ( 'NONE', *, *, #11753, .T. ) ;
#10126=CARTESIAN_POINT ( 'NONE',  ( 41.43369393131069245, -3.642920876114430495, -2.713652344655540727 ) ) ;
#10145=CARTESIAN_POINT ( 'NONE',  ( 19.01480233880806381, -3.011762293215139330, 0.07017451552781951707 ) ) ;
#10152=CARTESIAN_POINT ( 'NONE',  ( 54.97626768014088583, -6.471998454829187786, 4.043900691106972367 ) ) ;
#10187=CARTESIAN_POINT ( 'NONE',  ( 23.87614828266729461, -3.446665583135212874, 0.07017451549142075806 ) ) ;
#10200=CARTESIAN_POINT ( 'NONE',  ( 28.69289731897472961, -5.642913542083610956, -4.033870043669357308 ) ) ;
#10209=CARTESIAN_POINT ( 'NONE',  ( 102.9885081044300676, -6.698322160490901567, -0.07017451552783579571 ) ) ;
#10276=CARTESIAN_POINT ( 'NONE',  ( 84.65816297383790356, -6.961284151106942097, -0.07017451552783579571 ) ) ;
#10278=CARTESIAN_POINT ( 'NONE',  ( 29.27523314209665983, -3.695744416148424527, -0.07017451552781628354 ) ) ;
#10306=CARTESIAN_POINT ( 'NONE',  ( 29.18953645666585572, -9.308308156628573471, 1.010822989962089746 ) ) ;
#10341=CARTESIAN_POINT ( 'NONE',  ( 85.03004892703806661, -5.110667302027010805, 4.112223744664014191 ) ) ;
#10369=CARTESIAN_POINT ( 'NONE',  ( 18.92745801356193169, -3.988096551856957550, 2.787782631236393804 ) ) ;
#10375=CARTESIAN_POINT ( 'NONE',  ( 55.02116481234003942, -8.082960297853386322, 1.169950777205091663 ) ) ;
#10379=CARTESIAN_POINT ( 'NONE',  ( 29.38825086720287771, -3.456623792456554156, 2.713652344655542503 ) ) ;
#10385=CARTESIAN_POINT ( 'NONE',  ( 69.01493751667922538, -5.004537671629235795, -4.043901188646982447 ) ) ;
#10401=CARTESIAN_POINT ( 'NONE',  ( 18.86054332783663767, -4.736068442360261699, 3.993434336035624366 ) ) ;
#10446=CARTESIAN_POINT ( 'NONE',  ( 101.9216173105994159, -5.769792427975438898, -0.02339150517595088921 ) ) ;
#10449=CARTESIAN_POINT ( 'NONE',  ( 84.37491783462775174, -2.359815117480508651, 0.07017451552782423552 ) ) ;
#10450=CARTESIAN_POINT ( 'NONE',  ( 102.6609843814833027, -1.982062027707616192, 4.522129901861162260 ) ) ;
#10458=( LENGTH_UNIT ( ) NAMED_UNIT ( * ) SI_UNIT ( .MILLI., .METRE. ) );
#10462=CARTESIAN_POINT ( 'NONE',  ( 102.8769692529049564, -5.092190445904433815, -0.07017451552783644797 ) ) ;
#10472=CARTESIAN_POINT ( 'NONE',  ( 69.42401195566041849, -8.835509274224046194, 0.07017451552781803215 ) ) ;
#10479=CARTESIAN_POINT ( 'NONE',  ( 55.01406067017561696, -7.826279391976612487, -1.873789188487492430 ) ) ;
#10501=CARTESIAN_POINT ( 'NONE',  ( 18.77000516020590482, -5.748103448524430448, 4.150065909458478863 ) ) ;
#10523=CARTESIAN_POINT ( 'NONE',  ( 84.85832005755364094, -2.331047133796893878, 0.07017451552782270896 ) ) ;
#10524=CARTESIAN_POINT ( 'NONE',  ( 18.60860417056574079, -7.552242585353607929, 0.8105616806061413104 ) ) ;
#10536=CARTESIAN_POINT ( 'NONE',  ( 18.82056267271510208, -5.182971926406968244, -4.312042181581901445 ) ) ;
#10569=EDGE_CURVE ( 'NONE', #24800, #15472, #9728, .T. ) ;
#10571=DIRECTION ( 'NONE',  ( -0.9960221812693187404, 0.08910563629484180570, 0.000000000000000000 ) ) ;
#10602=CARTESIAN_POINT ( 'NONE',  ( 48.01729800609908949, -4.703650321867185902, 4.522129901861162260 ) ) ;
#10613=CARTESIAN_POINT ( 'NONE',  ( 102.5484925806840835, -0.3622080806379225915, -1.915219082070890755 ) ) ;
#10632=CARTESIAN_POINT ( 'NONE',  ( 69.13676591393821980, -7.435400085125419167, -1.873789664671283051 ) ) ;
#10653=CARTESIAN_POINT ( 'NONE',  ( 102.4142005201414918, -3.868549851786822646, 4.150065902002959106 ) ) ;
#10668=CARTESIAN_POINT ( 'NONE',  ( 102.5016417986325621, -5.123484090859097506, -2.184956770182200358 ) ) ;
#10669=ORIENTED_EDGE ( 'NONE', *, *, #22134, .F. ) ;
#10675=CARTESIAN_POINT ( 'NONE',  ( 102.6609843814833027, -1.982062027707616192, 4.522129901861162260 ) ) ;
#10679=CARTESIAN_POINT ( 'NONE',  ( 23.61221640758335027, -8.051464822112823327, 0.07017451552782230650 ) ) ;
#10686=CARTESIAN_POINT ( 'NONE',  ( 48.01729800609908949, -4.703650321870253670, 4.522129901861162260 ) ) ;
#10691=DIRECTION ( 'NONE',  ( 0.06927878976713386372, -0.9975973382524639943, 0.000000000000000000 ) ) ;
#10692=CARTESIAN_POINT ( 'NONE',  ( 102.3491787549029510, -2.929927866010495041, -4.093303780340187714 ) ) ;
#10743=CARTESIAN_POINT ( 'NONE',  ( 101.6022419886208610, -1.170867242066747416, 0.07017451552782490165 ) ) ;
#10748=VERTEX_POINT ( 'NONE', #21803 ) ;
#10757=CARTESIAN_POINT ( 'NONE',  ( 85.05927807847463384, -5.579234875942719718, 3.390607678642486800 ) ) ;
#10766=CARTESIAN_POINT ( 'NONE',  ( 23.90742340929273624, -3.204431202270332513, 2.713652344655542503 ) ) ;
#10772=B_SPLINE_CURVE_WITH_KNOTS ( 'NONE', 3,
 ( #23615, #13398, #28788, #18945, #1220, #20955 ),
 .UNSPECIFIED., .F., .F.,
 ( 4, 2, 4 ),
 ( 0.009536920346932657028, 0.5047684601734664378, 1.000000000000000000 ),
 .UNSPECIFIED. ) ;
#10776=ORIENTED_EDGE ( 'NONE', *, *, #15880, .F. ) ;
#10777=CARTESIAN_POINT ( 'NONE',  ( 23.95058674323790271, -2.449331254364353949, -0.07017451552781628354 ) ) ;
#10791=CARTESIAN_POINT ( 'NONE',  ( 68.92885037294648498, -3.291915072450345647, -0.8105619191593885775 ) ) ;
#10794=CARTESIAN_POINT ( 'NONE',  ( 18.51491971917342028, -8.599446730134173933, 0.07017451552781803215 ) ) ;
#10803=CARTESIAN_POINT ( 'NONE',  ( 69.14445055419099617, -7.589252662747979272, -1.529340293471085355 ) ) ;
#10804=CARTESIAN_POINT ( 'NONE',  ( 19.03654924710324892, -2.768675503676413019, -2.713652344655541615 ) ) ;
#10829=CARTESIAN_POINT ( 'NONE',  ( 54.97514302769123162, -6.431362512712788693, 4.093303786126267774 ) ) ;
#10849=CARTESIAN_POINT ( 'NONE',  ( 41.35430931302077795, -7.517178856329168823, -2.787783064041839953 ) ) ;
#10879=CARTESIAN_POINT ( 'NONE',  ( 102.3561127732198770, -3.030023377210125712, -4.185347658349727773 ) ) ;
#10922=CARTESIAN_POINT ( 'NONE',  ( 102.3439814245641344, -2.854902261435320110, -3.993434327320336319 ) ) ;
#10932=CARTESIAN_POINT ( 'NONE',  ( 18.69993402965692653, -6.531358056919786215, 2.942092882392380648 ) ) ;
#10935=CARTESIAN_POINT ( 'NONE',  ( 101.6022419886208610, -1.170867242066747416, 0.07017451552782490165 ) ) ;
#10939=CARTESIAN_POINT ( 'NONE',  ( 47.94319819119432680, -7.452467522312293369, 2.787782382152882654 ) ) ;
#10943=EDGE_LOOP ( 'NONE', ( #23843, #13435, #17830, #30090 ) ) ;
#10945=B_SPLINE_CURVE_WITH_KNOTS ( 'NONE', 3,
 ( #25284, #28269, #30661, #15393, #376, #12886 ),
 .UNSPECIFIED., .F., .F.,
 ( 4, 2, 4 ),
 ( 0.000000000000000000, 0.001111101129502802768, 0.002222202259005605536 ),
 .UNSPECIFIED. ) ;
#10977=CARTESIAN_POINT ( 'NONE',  ( 47.95525692263769457, -8.175714017047097215, -1.529339665925934177 ) ) ;
#10993=CARTESIAN_POINT ( 'NONE',  ( 40.87146290595926956, -4.622005974792367411, -2.184956282064931088 ) ) ;
#10998=CARTESIAN_POINT ( 'NONE',  ( 28.68200330691262323, -6.065191176973169895, 4.312042181588143563 ) ) ;
#11018=ORIENTED_EDGE ( 'NONE', *, *, #5217, .T. ) ;
#11025=CARTESIAN_POINT ( 'NONE',  ( 29.18511942701327300, -8.255514837368274073, 0.8105614686238012956 ) ) ;
#11031=CARTESIAN_POINT ( 'NONE',  ( 18.75828436637440433, -5.879118399754064583, 3.993434335971381532 ) ) ;
#11064=CARTESIAN_POINT ( 'NONE',  ( 47.75999538435752356, -8.435302152669851949, -0.07017451552783426916 ) ) ;
#11067=ORIENTED_EDGE ( 'NONE', *, *, #7297, .T. ) ;
#11075=CARTESIAN_POINT ( 'NONE',  ( 29.21519671786122885, -8.552672223070194590, -2.713652344655543391 ) ) ;
#11115=CARTESIAN_POINT ( 'NONE',  ( 47.88515715257229033, -3.977125052580343656, -1.169950612145078450 ) ) ;
#11123=CARTESIAN_POINT ( 'NONE',  ( 85.13967574987859166, -6.881122605236785539, -0.8105612905604291374 ) ) ;
#11144=CARTESIAN_POINT ( 'NONE',  ( 40.87951250943078918, -6.073635182929082887, 4.275175681039489639 ) ) ;
#11157=CARTESIAN_POINT ( 'NONE',  ( 18.75828436641558028, -5.879118399717574661, -3.993434336035625254 ) ) ;
#11160=EDGE_CURVE ( 'NONE', #22902, #6888, #15738, .T. ) ;
#11167=ORIENTED_EDGE ( 'NONE', *, *, #7888, .T. ) ;
#11180=CARTESIAN_POINT ( 'NONE',  ( 18.75839033845637971, -5.877933844985113510, 3.995336671754854407 ) ) ;
#11208=CARTESIAN_POINT ( 'NONE',  ( 18.73307111251037327, -6.160951975821718385, -3.539148371795089787 ) ) ;
#11248=CARTESIAN_POINT ( 'NONE',  ( 69.07074218556155643, -6.116471746203279380, 3.993434826126005088 ) ) ;
#11281=CARTESIAN_POINT ( 'NONE',  ( 41.34386496146564838, -3.886814715717100022, -0.07017451552238240797 ) ) ;
#11288=CARTESIAN_POINT ( 'NONE',  ( 101.8535835026724925, -4.790122518509368099, 2.790665559886620795 ) ) ;
#11311=ORIENTED_EDGE ( 'NONE', *, *, #15583, .F. ) ;
#11317=CARTESIAN_POINT ( 'NONE',  ( 18.84933643290985827, -4.861339035673776898, 4.155404940064419961 ) ) ;
#11320=EDGE_CURVE ( 'NONE', #28727, #11796, #6885, .T. ) ;
#11354=CARTESIAN_POINT ( 'NONE',  ( 85.10567447696165289, -6.328783234401409885, 2.184955974440073945 ) ) ;
#11363=CARTESIAN_POINT ( 'NONE',  ( 40.88398506880648142, -6.895404553204455667, 3.995336175096711795 ) ) ;
#11392=CARTESIAN_POINT ( 'NONE',  ( 101.8082167159056581, -4.136852074903159426, -3.842005631892731365 ) ) ;
#11410=CARTESIAN_POINT ( 'NONE',  ( 40.87775403842539390, -5.752705061965228239, -3.999773184981716412 ) ) ;
#11438=DIRECTION ( 'NONE',  ( 0.03662738895564519870, -0.5274252892134370096, 0.8488115212910427587 ) ) ;
#11456=CARTESIAN_POINT ( 'NONE',  ( 102.2233072702345282, -1.127920370132908578, -0.07017451552782009994 ) ) ;
#11487=CARTESIAN_POINT ( 'NONE',  ( 18.83159731376371937, -5.059626785736968557, 4.275175838856085875 ) ) ;
#11489=CARTESIAN_POINT ( 'NONE',  ( 28.68519643165576838, -5.941144522439076425, -4.275175838848107368 ) ) ;
#11520=ORIENTED_EDGE ( 'NONE', *, *, #25526, .T. ) ;
#11522=CARTESIAN_POINT ( 'NONE',  ( 40.88398722466511259, -6.895802492134996520, 3.994702139290142284 ) ) ;
#11534=VERTEX_POINT ( 'NONE', #23672 ) ;
#11562=CARTESIAN_POINT ( 'NONE',  ( 69.01325465695039441, -4.970808894665998068, -3.994703126863269560 ) ) ;
#11581=CARTESIAN_POINT ( 'NONE',  ( 41.44567272411835290, -7.615257740949710197, -4.522129901861164036 ) ) ;
#11596=CARTESIAN_POINT ( 'NONE',  ( 41.43369393131069245, -3.642920876114430495, -2.713652344655540727 ) ) ;
#11597=B_SPLINE_SURFACE_WITH_KNOTS ( 'NONE', 3, 3, ( 
 ( #17399, #6853, #19734, #4366, #30132, #32121, #14548, #24566, #2028, #24758 ),
 ( #29775, #27088, #17039, #12053, #9018, #1878, #4190, #26939, #27594, #22249 ),
 ( #6533, #32459, #1525, #4542, #11888, #9518, #22096, #14357, #27440, #4042 ),
 ( #17236, #25065, #12370, #16737, #11701, #14716, #12200, #1690, #22400, #6702 ),
 ( #32618, #2183, #9697, #31954, #19923, #7207, #19239, #4695, #29438, #14210 ),
 ( #24408, #21903, #9198, #19427, #29620, #18054, #22590, #32804, #10026, #17719 ),
 ( #27930, #10523, #22900, #2, #5349, #20236, #23245, #17902, #10187, #2682 ) ),
 .UNSPECIFIED., .F., .F., .F.,
 ( 4, 3, 4 ),
 ( 4, 3, 3, 4 ),
 ( -5.867317828880905293E-13, 0.4999999999997066236, 1.000000000000000000 ),
 ( 0.003598893295620731597, 0.5017994466482779137, 0.7508997233246064162, 1.000000000000935030 ),
 .UNSPECIFIED. ) ;
#11611=CARTESIAN_POINT ( 'NONE',  ( 101.8601177974632463, -4.884214737968172848, 2.639238349664508654 ) ) ;
#11638=CARTESIAN_POINT ( 'NONE',  ( 102.3474756592083850, -2.905342955644300673, 4.074610060380101650 ) ) ;
#11640=CARTESIAN_POINT ( 'NONE',  ( 18.78723038048999072, -5.555560056344673647, -4.275175838854464061 ) ) ;
#11659=VERTEX_POINT ( 'NONE', #23976 ) ;
#11665=CARTESIAN_POINT ( 'NONE',  ( 18.68265047573912341, -6.724553502642427461, -4.522129901861164036 ) ) ;
#11674=CARTESIAN_POINT ( 'NONE',  ( 69.07039640138465586, -6.115296054910306367, 3.995337163039132555 ) ) ;
#11701=CARTESIAN_POINT ( 'NONE',  ( 47.88515715254438021, -3.977125052580793518, 1.169950612146031466 ) ) ;
#11703=EDGE_LOOP ( 'NONE', ( #4078, #22800, #33031, #11018 ) ) ;
#11704=CARTESIAN_POINT ( 'NONE',  ( 101.7025720532070778, -2.615595213129288332, 3.539106238044632313 ) ) ;
#11708=CARTESIAN_POINT ( 'NONE',  ( 41.43369393131070666, -3.642920876109168926, -2.713652344655542503 ) ) ;
#11717=CARTESIAN_POINT ( 'NONE',  ( 84.96572415149093160, -4.061352282173294803, -3.997237729493234859 ) ) ;
#11744=ORIENTED_EDGE ( 'NONE', *, *, #2916, .F. ) ;
#11746=LINE ( 'NONE', #14100, #7147 ) ;
#11753=EDGE_CURVE ( 'NONE', #6454, #32072, #13517, .T. ) ;
#11796=VERTEX_POINT ( 'NONE', #32522 ) ;
#11801=ORIENTED_EDGE ( 'NONE', *, *, #29356, .F. ) ;
#11808=CARTESIAN_POINT ( 'NONE',  ( 40.88087200082812700, -6.322651088315213386, -4.312042181584450518 ) ) ;
#11820=CARTESIAN_POINT ( 'NONE',  ( 19.10390797508231131, -2.015740111943978619, -0.07017451552781628354 ) ) ;
#11828=CARTESIAN_POINT ( 'NONE',  ( 84.65816297383794620, -6.961284151106944762, 0.07017451552781739377 ) ) ;
#11849=CARTESIAN_POINT ( 'NONE',  ( 40.88390192208362350, -6.880058196568322515, 4.018749766545396618 ) ) ;
#11865=ORIENTED_EDGE ( 'NONE', *, *, #32853, .F. ) ;
#11888=CARTESIAN_POINT ( 'NONE',  ( 47.88685968119389003, -4.079890078784098151, 1.529339664924048048 ) ) ;
#11906=CARTESIAN_POINT ( 'NONE',  ( 54.94549555304173083, -5.360154568442904832, -3.994702633084190158 ) ) ;
#11911=CARTESIAN_POINT ( 'NONE',  ( 23.95058674323829706, -2.449331254355760823, 0.07017451552782173751 ) ) ;
#11933=CARTESIAN_POINT ( 'NONE',  ( 101.6058450947822109, -1.222751074449340614, -0.8125824203206647445 ) ) ;
#11943=ORIENTED_EDGE ( 'NONE', *, *, #7888, .F. ) ;
#11983=ORIENTED_EDGE ( 'NONE', *, *, #2916, .T. ) ;
#11989=CARTESIAN_POINT ( 'NONE',  ( 102.3922829939881325, -3.552157972614133907, -4.312042181587000478 ) ) ;
#11996=CARTESIAN_POINT ( 'NONE',  ( 101.7460786050199033, -3.242078736165208586, 4.282223226228373036 ) ) ;
#12000=EDGE_CURVE ( 'NONE', #25815, #31589, #9669, .T. ) ;
#12001=CARTESIAN_POINT ( 'NONE',  ( 41.43141396789281572, -2.886852813804338780, -0.07017451552781628354 ) ) ;
#12023=ORIENTED_EDGE ( 'NONE', *, *, #3089, .F. ) ;
#12025=CARTESIAN_POINT ( 'NONE',  ( 102.4221483139552191, -3.983281035618068344, 4.018750258902361594 ) ) ;
#12040=CARTESIAN_POINT ( 'NONE',  ( 85.08949032934707191, -1.315411135598756553, 0.07017451552782173751 ) ) ;
#12053=CARTESIAN_POINT ( 'NONE',  ( 54.90853374638842865, -4.039626021003883238, 1.873789188464484390 ) ) ;
#12068=CARTESIAN_POINT ( 'NONE',  ( 54.94551756700143841, -5.360949955573579118, -3.995970705067843909 ) ) ;
#12072=CARTESIAN_POINT ( 'NONE',  ( 102.5829460782277351, -0.8583298743146012821, 2.713652344655541615 ) ) ;
#12104=VERTEX_POINT ( 'NONE', #29295 ) ;
#12112=CARTESIAN_POINT ( 'NONE',  ( 102.6609843814833027, -1.982062027707615526, -4.522129901861162260 ) ) ;
#12122=CARTESIAN_POINT ( 'NONE',  ( 35.23476908784418526, -3.791088091780328906, 0.07017451550800198057 ) ) ;
#12123=CARTESIAN_POINT ( 'NONE',  ( 18.68265047573912341, -6.724553502642427461, 4.522129901861163148 ) ) ;
#12139=CARTESIAN_POINT ( 'NONE',  ( 28.66985322744200815, -6.539611658422689544, -4.215290389460269793 ) ) ;
#12154=CARTESIAN_POINT ( 'NONE',  ( 85.13613392229179055, -2.069934983084471103, -2.713652344655540727 ) ) ;
#12164=CARTESIAN_POINT ( 'NONE',  ( 48.05280571049738825, -6.817569152029394175, -5.695980980372493008 ) ) ;
#12172=CARTESIAN_POINT ( 'NONE',  ( 85.03499643008539977, -5.191404901269152106, 4.013697181026976146 ) ) ;
#12200=CARTESIAN_POINT ( 'NONE',  ( 35.33972979713486495, -3.946928302550552825, 1.169950777404600739 ) ) ;
#12212=CARTESIAN_POINT ( 'NONE',  ( 28.69339080511027973, -5.623844247569588894, -4.006107076269940670 ) ) ;
#12218=CARTESIAN_POINT ( 'NONE',  ( 85.48138648428260922, -7.654866896025225742, -1.915219082070897638 ) ) ;
#12257=CARTESIAN_POINT ( 'NONE',  ( 54.91389575944440793, -4.233367447934999639, -2.184956776131685707 ) ) ;
#12261=CARTESIAN_POINT ( 'NONE',  ( 85.20563808598696198, -3.194259795296082061, -4.522129901861162260 ) ) ;
#12275=CARTESIAN_POINT ( 'NONE',  ( 85.38119660045754244, -6.034158634414237277, 4.522129901861163148 ) ) ;
#12296=CARTESIAN_POINT ( 'NONE',  ( 18.80941384712907904, -5.307593421025357472, -4.312042181584450518 ) ) ;
#12301=CARTESIAN_POINT ( 'NONE',  ( 101.7221769401408551, -2.897900707893039662, 3.993434276071444078 ) ) ;
#12309=CARTESIAN_POINT ( 'NONE',  ( 101.6572086713194665, -1.962373798936464242, -2.487845072520846301 ) ) ;
#12321=CARTESIAN_POINT ( 'NONE',  ( 23.72239361537270241, -6.441344918482257320, -5.695980980372493008 ) ) ;
#12327=CARTESIAN_POINT ( 'NONE',  ( 18.97846294920043420, -3.417963736896675986, 1.868788737152642598 ) ) ;
#12336=CARTESIAN_POINT ( 'NONE',  ( 28.66422432450819358, -6.760491130759657352, 4.001040682715384378 ) ) ;
#12351=CARTESIAN_POINT ( 'NONE',  ( 41.43141396789280151, -2.886852813799071438, 0.07017451552782173751 ) ) ;
#12365=CARTESIAN_POINT ( 'NONE',  ( 18.89400067069965772, -4.362082497104407430, 3.390608483629235614 ) ) ;
#12370=CARTESIAN_POINT ( 'NONE',  ( 68.93397511290362445, -3.394585223421699549, 1.169951107274293856 ) ) ;
#12383=CARTESIAN_POINT ( 'NONE',  ( 54.94602868030273868, -5.379417012101376017, -4.023790190284213253 ) ) ;
#12457=ADVANCED_FACE ( 'NONE', ( #20443 ), #525, .T. ) ;
#12474=CARTESIAN_POINT ( 'NONE',  ( 101.7699185271994224, -3.585367684922579290, -4.312036717292317967 ) ) ;
#12495=CARTESIAN_POINT ( 'NONE',  ( 102.5829460782277351, -0.8583298743145996168, -2.713652344655541615 ) ) ;
#12519=CARTESIAN_POINT ( 'NONE',  ( 40.88395664866006740, -6.890158765445390188, 4.003574183511678264 ) ) ;
#12533=CARTESIAN_POINT ( 'NONE',  ( 85.03618457008526832, -5.204454441919745378, -3.993433531025833982 ) ) ;
#12543=CARTESIAN_POINT ( 'NONE',  ( 18.86054332783663767, -4.736068442360261699, 3.993434336035624366 ) ) ;
#12548=CARTESIAN_POINT ( 'NONE',  ( 41.44567272411835290, -7.615257740949710197, 4.522129901861162260 ) ) ;
#12557=CARTESIAN_POINT ( 'NONE',  ( 54.94593103970883163, -5.375889154831037686, -4.018750264957798635 ) ) ;
#12558=ORIENTED_EDGE ( 'NONE', *, *, #8565, .F. ) ;
#12563=CARTESIAN_POINT ( 'NONE',  ( 69.41104820195521086, -8.577144703210709764, -1.915219082070897638 ) ) ;
#12570=DIRECTION ( 'NONE',  ( -0.03662738895564521951, 0.5274252892134372317, -0.8488115212910425367 ) ) ;
#12614=CARTESIAN_POINT ( 'NONE',  ( 23.58234648083524121, -8.048792613698569909, 0.02339150517593243869 ) ) ;
#12616=CARTESIAN_POINT ( 'NONE',  ( 101.6022419886208610, -1.170867242066748304, -0.02339150518254430253 ) ) ;
#12646=CARTESIAN_POINT ( 'NONE',  ( 85.38119660046028514, -6.034158634444421132, 4.522129901861162260 ) ) ;
#12648=CARTESIAN_POINT ( 'NONE',  ( 47.99837860531643940, -3.577301031424836353, -2.713652344655540727 ) ) ;
#12663=ORIENTED_EDGE ( 'NONE', *, *, #20313, .F. ) ;
#12666=EDGE_LOOP ( 'NONE', ( #16535, #6663, #25312, #26789 ) ) ;
#12669=CARTESIAN_POINT ( 'NONE',  ( 28.66479303568530312, -6.738141520292279196, 4.033870043683038809 ) ) ;
#12681=ORIENTED_EDGE ( 'NONE', *, *, #32303, .T. ) ;
#12709=CARTESIAN_POINT ( 'NONE',  ( 28.69308027625054436, -5.635843304107821972, -4.023790193015413408 ) ) ;
#12754=CARTESIAN_POINT ( 'NONE',  ( 18.68312535291511267, -6.719245328341675538, 2.639238440967430321 ) ) ;
#12755=CARTESIAN_POINT ( 'NONE',  ( 29.18953645666585217, -9.308308156628569918, 0.07017451552781736601 ) ) ;
#12761=FACE_OUTER_BOUND ( 'NONE', #23322, .T. ) ;
#12764=CARTESIAN_POINT ( 'NONE',  ( 23.84310522038115465, -4.329614468541457484, 4.522129901861162260 ) ) ;
#12772=CARTESIAN_POINT ( 'NONE',  ( 18.77131501682890757, -5.733461880277683775, -4.171847256157208861 ) ) ;
#12777=CARTESIAN_POINT ( 'NONE',  ( 18.60402535543785518, -7.603424548862136589, 0.02339150517593243869 ) ) ;
#12787=CARTESIAN_POINT ( 'NONE',  ( 18.58227844715246135, -7.846511338401735536, 2.713652344655544724 ) ) ;
#12796=CARTESIAN_POINT ( 'NONE',  ( 101.6962914994147411, -2.525156800924736267, -3.393559278664259882 ) ) ;
#12818=CARTESIAN_POINT ( 'NONE',  ( 40.88384453718996525, -6.869468092516608060, 4.033869542149528087 ) ) ;
#12849=CARTESIAN_POINT ( 'NONE',  ( 68.99418471616174031, -4.594926857588857771, 3.390608975014814064 ) ) ;
#12851=CARTESIAN_POINT ( 'NONE',  ( 18.75828436641558028, -5.879118399717575549, 3.993434336035622589 ) ) ;
#12861=CARTESIAN_POINT ( 'NONE',  ( 47.99837860531645362, -3.577301031424839017, 2.713652344655542503 ) ) ;
#12866=CARTESIAN_POINT ( 'NONE',  ( 69.01361805596027921, -4.978092444658805960, -4.006107570160923892 ) ) ;
#12875=EDGE_CURVE ( 'NONE', #10748, #30917, #4665, .T. ) ;
#12876=DIRECTION ( 'NONE',  ( -0.9975973382524639943, -0.06927878976713693071, 0.000000000000000000 ) ) ;
#12886=CARTESIAN_POINT ( 'NONE',  ( 18.60402535543785518, -7.603424548862136589, -0.07017451552783579571 ) ) ;
#12916=CARTESIAN_POINT ( 'NONE',  ( 18.58227844715246135, -7.846511338401735536, 2.713652344655544724 ) ) ;
#12921=EDGE_CURVE ( 'NONE', #5699, #21989, #16602, .T. ) ;
#12930=CARTESIAN_POINT ( 'NONE',  ( 18.67472101454464450, -6.813188964052660168, 2.487811220254955380 ) ) ;
#12946=CARTESIAN_POINT ( 'NONE',  ( 18.60402535543785518, -7.603424548862136589, -0.07017451552783579571 ) ) ;
#12964=CARTESIAN_POINT ( 'NONE',  ( 23.95058674323829706, -2.449331254355760823, -0.07017451552781585333 ) ) ;
#12977=CARTESIAN_POINT ( 'NONE',  ( 23.58793147791972444, -8.793627369988312736, 1.915219082070893863 ) ) ;
#12987=CARTESIAN_POINT ( 'NONE',  ( 102.5153059484011919, -5.316817625850402962, -1.873789182721711688 ) ) ;
#13007=CARTESIAN_POINT ( 'NONE',  ( 54.94526044243337282, -5.359369332727098367, -3.993434333344310083 ) ) ;
#13013=CARTESIAN_POINT ( 'NONE',  ( 54.97462353180808492, -6.412592106988439511, 4.112224493134436720 ) ) ;
#13046=CARTESIAN_POINT ( 'NONE',  ( 35.27427105688962428, -8.145327135409177188, 1.529339875372225155 ) ) ;
#13058=CARTESIAN_POINT ( 'NONE',  ( 102.3749895180278884, -3.302517831782471269, -4.312042181581901445 ) ) ;
#13087=ORIENTED_EDGE ( 'NONE', *, *, #2953, .T. ) ;
#13090=CARTESIAN_POINT ( 'NONE',  ( 84.62099044691944982, -6.357652361253733453, -2.184954680052196174 ) ) ;
#13118=CARTESIAN_POINT ( 'NONE',  ( 102.7116376760607039, -2.711456868667909692, 5.695980980372492120 ) ) ;
#13127=CARTESIAN_POINT ( 'NONE',  ( 85.08949032934707191, -1.315411135598751668, -1.010822989962086416 ) ) ;
#13138=CARTESIAN_POINT ( 'NONE',  ( 18.51491971917342028, -8.599446730134175709, 1.010822989962089746 ) ) ;
#13146=CARTESIAN_POINT ( 'NONE',  ( 69.12709522372691140, -7.241778149835380596, -2.184957268579761802 ) ) ;
#13160=CARTESIAN_POINT ( 'NONE',  ( 18.89400067069844624, -4.362082497106836598, -3.390608483633292813 ) ) ;
#13165=CARTESIAN_POINT ( 'NONE',  ( 28.66518199730131755, -6.722860712036216491, 4.053847714221102905 ) ) ;
#13179=CARTESIAN_POINT ( 'NONE',  ( 102.4497391607709886, -4.374320780254121743, -3.390608474985632448 ) ) ;
#13191=EDGE_CURVE ( 'NONE', #8159, #19057, #4526, .T. ) ;
#13199=CARTESIAN_POINT ( 'NONE',  ( 40.87951250946358783, -6.073635182903602825, -4.275175681028137831 ) ) ;
#13206=CARTESIAN_POINT ( 'NONE',  ( 18.53796472816966556, -8.341849780241110679, -1.915219082070897638 ) ) ;
#13210=CARTESIAN_POINT ( 'NONE',  ( 40.74410603220348293, -8.021703207543309233, 2.184955501613824236 ) ) ;
#13224=CARTESIAN_POINT ( 'NONE',  ( 101.8278197859226708, -4.419131406518054916, -3.387719699150975927 ) ) ;
#13235=CARTESIAN_POINT ( 'NONE',  ( 69.42401195566040428, -8.835509274236315491, -0.07017451552783579571 ) ) ;
#13251=CARTESIAN_POINT ( 'NONE',  ( 18.70833836802739469, -6.437414421208801585, 3.093520103104856034 ) ) ;
#13253=LINE ( 'NONE', #28798, #13884 ) ;
#13254=CARTESIAN_POINT ( 'NONE',  ( 101.6058569626687245, -1.222921969063083258, 0.8134928172057650508 ) ) ;
#13263=CARTESIAN_POINT ( 'NONE',  ( 48.02957825751263243, -5.434743900606504141, 5.695980980372492120 ) ) ;
#13271=CARTESIAN_POINT ( 'NONE',  ( 18.79913864311901861, -5.422449579812291809, -4.312036717478699543 ) ) ;
#13276=CARTESIAN_POINT ( 'NONE',  ( 101.6441386174529384, -1.774168274679073454, -2.184956718804114573 ) ) ;
#13282=CARTESIAN_POINT ( 'NONE',  ( 68.92628806523701712, -3.240579989648070036, -0.07017451552797518421 ) ) ;
#13284=CARTESIAN_POINT ( 'NONE',  ( 69.38611993481310947, -8.080330187051606217, 2.713652344655544724 ) ) ;
#13293=CARTESIAN_POINT ( 'NONE',  ( 85.10567447696169552, -6.328783234401409885, -2.184955974440073501 ) ) ;
#13313=CARTESIAN_POINT ( 'NONE',  ( 102.4180935425471972, -3.924747953286301438, 4.093303780333640951 ) ) ;
#13340=CARTESIAN_POINT ( 'NONE',  ( 41.35712849199997976, -8.497574858407940468, 0.07017451552782413837 ) ) ;
#13353=CARTESIAN_POINT ( 'NONE',  ( 102.3504764446131645, -2.948660565431382885, -4.112224487563005404 ) ) ;
#13375=CARTESIAN_POINT ( 'NONE',  ( 102.9361373302715918, -5.944196040818415128, -2.713652344655542947 ) ) ;
#13396=B_SPLINE_CURVE_WITH_KNOTS ( 'NONE', 3,
 ( #5435, #576, #33023, #18304, #20980, #26152, #10766, #15442 ),
 .UNSPECIFIED., .F., .F.,
 ( 4, 2, 2, 4 ),
 ( 0.000000000000000000, 0.5000000000000000000, 0.7500000000000000000, 1.000000000000000000 ),
 .UNSPECIFIED. ) ;
#13398=CARTESIAN_POINT ( 'NONE',  ( 84.48140976240925681, -4.087790770811431607, 3.993432235017919218 ) ) ;
#13415=ADVANCED_FACE ( 'NONE', ( #3252 ), #653, .F. ) ;
#13435=ORIENTED_EDGE ( 'NONE', *, *, #30202, .F. ) ;
#13436=CARTESIAN_POINT ( 'NONE',  ( 23.93581954898842667, -2.707668749993698665, -1.915219082070890755 ) ) ;
#13448=CARTESIAN_POINT ( 'NONE',  ( 47.88345462391697538, -3.874360026377135391, -0.8105615593670084662 ) ) ;
#13458=VERTEX_POINT ( 'NONE', #19460 ) ;
#13461=CARTESIAN_POINT ( 'NONE',  ( 85.13336101766863351, -6.778540831288875523, -1.169950242242265848 ) ) ;
#13471=CARTESIAN_POINT ( 'NONE',  ( 68.97545755171020687, -4.219822329617093359, 2.787783122621469989 ) ) ;
#13491=CARTESIAN_POINT ( 'NONE',  ( 28.69228937106727528, -5.666394676789348495, 4.074610069494389641 ) ) ;
#13506=CARTESIAN_POINT ( 'NONE',  ( 18.64036474502219320, -7.197223105236783880, 1.868788737059465799 ) ) ;
#13507=CARTESIAN_POINT ( 'NONE',  ( 47.94319819119471049, -7.452467522295798119, -2.787782382176030360 ) ) ;
#13517=CIRCLE ( 'NONE', #32764, 1.676012832569465205 ) ;
#13522=CARTESIAN_POINT ( 'NONE',  ( 55.02542983044659763, -8.237060396196271839, 0.4367666027049950661 ) ) ;
#13531=CARTESIAN_POINT ( 'NONE',  ( 40.88398618353106428, -6.895614549178633368, 3.995006151606554479 ) ) ;
#13565=CARTESIAN_POINT ( 'NONE',  ( 18.65791233782715963, -7.001076235476726417, -2.184956778830003277 ) ) ;
#13573=CARTESIAN_POINT ( 'NONE',  ( 19.01480233880806381, -3.011762293215139330, 0.07017451552781951707 ) ) ;
#13577=FACE_OUTER_BOUND ( 'NONE', #4918, .T. ) ;
#13606=( NAMED_UNIT ( * ) SI_UNIT ( $, .STERADIAN. ) SOLID_ANGLE_UNIT ( ) );
#13620=CARTESIAN_POINT ( 'NONE',  ( 102.2268587688198664, -1.179183864763411416, -0.8105616763788804358 ) ) ;
#13626=DIRECTION ( 'NONE',  ( 0.06927878976713386372, -0.9975973382524639943, 0.000000000000000000 ) ) ;
#13631=CARTESIAN_POINT ( 'NONE',  ( 47.95270804829431910, -8.021719045402210924, -1.873788950395596897 ) ) ;
#13647=CARTESIAN_POINT ( 'NONE',  ( 40.87351160866354149, -4.997573076401069514, -2.787782134466627149 ) ) ;
#13652=CARTESIAN_POINT ( 'NONE',  ( 102.4008411508974064, -3.675699656476595578, 4.275175836083139558 ) ) ;
#13659=CARTESIAN_POINT ( 'NONE',  ( 18.77131732058334279, -5.733436128961898248, 4.171867820445585018 ) ) ;
#13666=CARTESIAN_POINT ( 'NONE',  ( 18.65791233782715963, -7.001076235476726417, -2.184956778830005053 ) ) ;
#13668=ORIENTED_EDGE ( 'NONE', *, *, #29969, .F. ) ;
#13680=CARTESIAN_POINT ( 'NONE',  ( 69.14957877370534334, -7.691922716132707727, 1.169951105759795329 ) ) ;
#13687=CARTESIAN_POINT ( 'NONE',  ( 18.75837163099988558, -5.878142956378915152, 3.995006647689397283 ) ) ;
#13693=ORIENTED_EDGE ( 'NONE', *, *, #9825, .T. ) ;
#13709=CARTESIAN_POINT ( 'NONE',  ( 101.9216173105994443, -5.769792427975438009, 0.07017451552781736601 ) ) ;
#13715=B_SPLINE_SURFACE_WITH_KNOTS ( 'NONE', 3, 3, ( 
 ( #10922, #13880, #4382, #4201, #14371, #6866, #14068 ),
 ( #16404, #21920, #26953, #4057, #1217, #32140, #24273 ),
 ( #9035, #1387, #11562, #11906, #6368, #1708, #22110 ),
 ( #24579, #16560, #9214, #32324, #21759, #31966, #27263 ),
 ( #32472, #26612, #3716, #12068, #17056, #22263, #9382 ),
 ( #19443, #29635, #14568, #19592, #19252, #27100, #24773 ),
 ( #6716, #11717, #16907, #29282, #26774, #1893, #29454 ),
 ( #29791, #9534, #24090, #6554, #16752, #19748, #14223 ),
 ( #24421, #3892, #6217, #1538, #11410, #21607, #31812 ),
 ( #8883, #19092, #27454, #25268, #28104, #22760, #7222 ),
 ( #7528, #24927, #5202, #2385, #15377, #2040, #10037 ),
 ( #2195, #14729, #12866, #2539, #30641, #12212, #15228 ),
 ( #25585, #22418, #20424, #30293, #32630, #2696, #9886 ),
 ( #23089, #7040, #4710, #4556, #210, #27943, #5051 ),
 ( #14879, #17412, #17251, #12557, #17558, #27756, #9711 ),
 ( #25081, #25431, #32815, #12383, #22603, #12709, #30145 ),
 ( #22911, #20102, #17, #27607, #32969, #10200, #7368 ),
 ( #17913, #4864, #10385, #19938, #15048, #29949, #7720 ),
 ( #20248, #30450, #17734, #23563, #29360, #26685, #25937 ),
 ( #6450, #15732, #5549, #16656, #1464, #7871, #15876 ),
 ( #10692, #21685, #3191, #19168, #5363, #20902, #23402 ),
 ( #13353, #24350, #23257, #687, #13969, #26865, #29205 ),
 ( #3983, #20594, #19021, #28604, #14152, #31125, #30803 ),
 ( #10879, #21087, #8214, #26086, #18413, #31288, #5698 ),
 ( #8816, #18063, #20747, #6295, #28252, #16479, #15547 ),
 ( #3800, #25764, #507, #18224, #13199, #11489, #24189 ),
 ( #13058, #1314, #8957, #31891, #2893, #360, #10536 ),
 ( #30946, #8025, #28437, #3044, #11808, #9119, #12296 ),
 ( #11989, #1968, #27362, #32238, #17152, #7293, #9618 ),
 ( #1804, #14962, #1615, #9302, #29867, #27181, #11640 ),
 ( #19518, #16981, #9806, #22016, #32551, #12139, #4479 ),
 ( #6794, #29714, #20027, #25176, #32048, #6950, #22509 ),
 ( #9457, #14653, #4786, #19349, #22339, #27531, #24496 ),
 ( #4287, #19674, #14462, #24850, #24678, #22187, #19843 ) ),
 .UNSPECIFIED., .F., .F., .F.,
 ( 4, 3, 3, 3, 3, 3, 3, 3, 3, 3, 3, 4 ),
 ( 4, 3, 4 ),
 ( -1.834560091635544504E-11, 0.001953124981690232886, 0.003906249981726066852, 0.007812499981797734784, 0.01562499998194107065, 0.03124999998222774064, 0.06249999998280108410, 0.1249999999839477710, 0.2499999999862411448, 0.4999999999908278925, 0.7499999999954145569, 1.000000000000001332 ),
 ( 0.003589107913150553671, 0.5017945539565752400, 1.000000000000000000 ),
 .UNSPECIFIED. ) ;
#13746=CARTESIAN_POINT ( 'NONE',  ( 18.80941384712784981, -5.307593421039076276, 3.636029349014984202 ) ) ;
#13760=LINE ( 'NONE', #31847, #31103 ) ;
#13766=B_SPLINE_CURVE_WITH_KNOTS ( 'NONE', 3,
 ( #23326, #26010, #7793, #8287, #18480, #13271, #5276, #12772, #101, #17822 ),
 .UNSPECIFIED., .F., .F.,
 ( 4, 2, 2, 2, 4 ),
 ( 0.000000000000000000, 0.0003410363541725900923, 0.0006820727083451801846, 0.001023109062517770385, 0.001364145416690360369 ),
 .UNSPECIFIED. ) ;
#13777=CARTESIAN_POINT ( 'NONE',  ( 35.27024661284173845, -8.402227462205928532, -0.07017451552783472712 ) ) ;
#13778=DIRECTION ( 'NONE',  ( -0.9960221812693187404, 0.08910563629484180570, 0.000000000000000000 ) ) ;
#13796=CARTESIAN_POINT ( 'NONE',  ( 54.94895328793697331, -5.485086176145982151, 4.155404937709241686 ) ) ;
#13810=CARTESIAN_POINT ( 'NONE',  ( 18.60402535544292490, -7.603424548862588672, 0.07017451552782096036 ) ) ;
#13818=CARTESIAN_POINT ( 'NONE',  ( 48.01729800609908949, -4.703650321867185902, 4.522129901861162260 ) ) ;
#13826=CARTESIAN_POINT ( 'NONE',  ( 102.5019105821284313, -5.123465467906984649, 2.184956770195073616 ) ) ;
#13840=ORIENTED_EDGE ( 'NONE', *, *, #2731, .T. ) ;
#13880=CARTESIAN_POINT ( 'NONE',  ( 84.96557803822885546, -4.058969597092461079, -3.993433529893592571 ) ) ;
#13881=ORIENTED_EDGE ( 'NONE', *, *, #2953, .F. ) ;
#13884=VECTOR ( 'NONE', #23453, 1000.000000000000000 ) ;
#13918=CARTESIAN_POINT ( 'NONE',  ( 19.03654924710324181, -2.768675503676409466, -2.713652344655540727 ) ) ;
#13926=CARTESIAN_POINT ( 'NONE',  ( 41.34386496146469625, -3.886814715719084656, -0.4367667078930305147 ) ) ;
#13940=CARTESIAN_POINT ( 'NONE',  ( 18.60402535544292490, -7.603424548862588672, -0.07017451552783671165 ) ) ;
#13965=CARTESIAN_POINT ( 'NONE',  ( 40.88276903860496247, -6.671230418110412508, 4.215290092866328386 ) ) ;
#13969=CARTESIAN_POINT ( 'NONE',  ( 40.87824777906663343, -5.842713490123291109, -4.112224033464637607 ) ) ;
#13971=B_SPLINE_CURVE_WITH_KNOTS ( 'NONE', 3,
 ( #15370, #28244, #15036, #27746, #198, #28098 ),
 .UNSPECIFIED., .F., .F.,
 ( 4, 2, 4 ),
 ( 0.009541643435016610234, 0.5047708217175083112, 1.000000000000000000 ),
 .UNSPECIFIED. ) ;
#13978=CARTESIAN_POINT ( 'NONE',  ( 18.89383689343546280, -4.363913198432375573, -3.393559380852849028 ) ) ;
#14006=CARTESIAN_POINT ( 'NONE',  ( 18.64064227445971866, -7.194120883405200395, 1.873789191074036964 ) ) ;
#14054=CARTESIAN_POINT ( 'NONE',  ( 101.7091070155185690, -2.709697044720575931, 3.690548917384798955 ) ) ;
#14058=ADVANCED_FACE ( 'NONE', ( #7956 ), #5316, .T. ) ;
#14068=CARTESIAN_POINT ( 'NONE',  ( 18.86054332783762177, -4.736068442332642903, -3.993434335991318473 ) ) ;
#14092=CARTESIAN_POINT ( 'NONE',  ( 85.38119660045754244, -6.034158634414237277, -4.522129901861164036 ) ) ;
#14100=CARTESIAN_POINT ( 'NONE',  ( 102.8580990270160385, -4.820463887425400884, -4.522129901861163148 ) ) ;
#14108=DIRECTION ( 'NONE',  ( 0.000000000000000000, 0.000000000000000000, -1.000000000000000000 ) ) ;
#14122=CARTESIAN_POINT ( 'NONE',  ( 101.9038780646438056, -5.514351699183295707, 1.526432238275731379 ) ) ;
#14123=CARTESIAN_POINT ( 'NONE',  ( 102.7595417042496706, -3.401262957566509204, -3.636029349014984202 ) ) ;
#14150=CARTESIAN_POINT ( 'NONE',  ( 40.87896744410521421, -5.974071964853076899, 4.215290092884966811 ) ) ;
#14152=CARTESIAN_POINT ( 'NONE',  ( 40.87845373110570080, -5.880277441428658491, -4.150065482907210779 ) ) ;
#14155=EDGE_LOOP ( 'NONE', ( #20344, #23556, #17388, #16112 ) ) ;
#14173=CARTESIAN_POINT ( 'NONE',  ( 29.25343337322282622, -7.426690278353109242, -4.522129901861164036 ) ) ;
#14210=CARTESIAN_POINT ( 'NONE',  ( 19.01022352368274326, -3.062944256723961534, 0.8105616806065999436 ) ) ;
#14223=CARTESIAN_POINT ( 'NONE',  ( 18.86025921852518650, -4.739244214245537101, -3.998506281407207208 ) ) ;
#14329=CARTESIAN_POINT ( 'NONE',  ( 102.4230704567010264, -3.996592730545043715, 3.998506272702885056 ) ) ;
#14342=DIRECTION ( 'NONE',  ( -0.9960221812693187404, 0.08910563629484180570, 0.000000000000000000 ) ) ;
#14357=CARTESIAN_POINT ( 'NONE',  ( 29.33166896507317389, -3.955587949931067993, 1.529339504158915064 ) ) ;
#14359=EDGE_LOOP ( 'NONE', ( #13087, #18132, #7852, #28102 ) ) ;
#14360=CARTESIAN_POINT ( 'NONE',  ( 102.9885081044300676, -6.698322160490901567, -0.07017451552783579571 ) ) ;
#14371=CARTESIAN_POINT ( 'NONE',  ( 40.87773210429867987, -5.748708618940125525, -3.993433839915444761 ) ) ;
#14375=CARTESIAN_POINT ( 'NONE',  ( 41.43141396789279440, -2.886852813799070105, 1.010822989962091301 ) ) ;
#14462=CARTESIAN_POINT ( 'NONE',  ( 69.07045576167539025, -6.116484151751043541, -3.993434826750828837 ) ) ;
#14479=CARTESIAN_POINT ( 'NONE',  ( 41.43141396789281572, -2.886852813804338780, 0.07017451552781951707 ) ) ;
#14507=CARTESIAN_POINT ( 'NONE',  ( 18.75871281239513166, -5.874329233548843732, 4.001040682667124315 ) ) ;
#14548=CARTESIAN_POINT ( 'NONE',  ( 35.33267181912139421, -4.397467831973882468, 2.184956776455081240 ) ) ;
#14551=CARTESIAN_POINT ( 'NONE',  ( 101.6441386174529953, -1.774168274679931212, 2.184956718805492581 ) ) ;
#14568=CARTESIAN_POINT ( 'NONE',  ( 69.01331421734823834, -4.972002658698717603, -3.996605157047315338 ) ) ;
#14572=CARTESIAN_POINT ( 'NONE',  ( 19.03654924710325602, -2.768675503676416572, 2.713652344655541615 ) ) ;
#14616=CARTESIAN_POINT ( 'NONE',  ( 102.2651039925858072, -1.731228206879547704, -2.184956770111041280 ) ) ;
#14631=FACE_OUTER_BOUND ( 'NONE', #10943, .T. ) ;
#14646=CARTESIAN_POINT ( 'NONE',  ( 101.7777806943559114, -3.698580936114888917, -4.282223226319369580 ) ) ;
#14653=CARTESIAN_POINT ( 'NONE',  ( 85.03270493638194694, -5.154008962840147312, -4.074609222412457932 ) ) ;
#14660=CARTESIAN_POINT ( 'NONE',  ( 101.7264006491828638, -2.958721067370967184, 4.091315454821516262 ) ) ;
#14679=CARTESIAN_POINT ( 'NONE',  ( 18.87102749435251425, -4.618876501924994216, -5.695980980372493008 ) ) ;
#14686=( BOUNDED_SURFACE ( )  B_SPLINE_SURFACE ( 3, 3, ( 
 ( #6929, #12275, #25339, #9438, #17128, #1951, #32703, #12123 ),
 ( #27664, #2272, #5112, #15627, #10096, #25844, #18125, #30713 ),
 ( #13118, #2962, #278, #13263, #2771, #18472, #28664, #25652 ),
 ( #10450, #15289, #7607, #10602, #28165, #28514, #12764, #3109 ) ),
 .UNSPECIFIED., .F., .F., .F. ) 
 B_SPLINE_SURFACE_WITH_KNOTS ( ( 4, 4 ),
 ( 4, 2, 2, 4 ),
 ( 0.000000000000000000, 1.000000000000000000 ),
 ( 0.000000000000000000, 0.5000000000000000000, 0.7500000000000000000, 1.000000000000000000 ),
 .UNSPECIFIED. ) 
 GEOMETRIC_REPRESENTATION_ITEM ( )  RATIONAL_B_SPLINE_SURFACE ( (
 ( 1.000000000000000000, 1.000000000000000000, 1.000000000000000000, 1.000000000000000000, 1.000000000000000000, 1.000000000000000000, 1.000000000000000000, 1.000000000000000000),
 ( 0.6857970438836927807, 0.6857970438836927807, 0.6857970438836927807, 0.6857970438836927807, 0.6857970438836927807, 0.6857970438836927807, 0.6857970438836927807, 0.6857970438836927807),
 ( 0.6857970438836927807, 0.6857970438836927807, 0.6857970438836927807, 0.6857970438836927807, 0.6857970438836927807, 0.6857970438836927807, 0.6857970438836927807, 0.6857970438836927807),
 ( 1.000000000000000000, 1.000000000000000000, 1.000000000000000000, 1.000000000000000000, 1.000000000000000000, 1.000000000000000000, 1.000000000000000000, 1.000000000000000000) ) ) 
 REPRESENTATION_ITEM ( '' )  SURFACE ( )  );
#14689=CARTESIAN_POINT ( 'NONE',  ( 28.66430776624534715, -6.757211549878646473, 4.006107076289154634 ) ) ;
#14702=CARTESIAN_POINT ( 'NONE',  ( 18.96044790064761898, -3.619335823787583006, -0.07017451552783579571 ) ) ;
#14716=CARTESIAN_POINT ( 'NONE',  ( 41.34428855215830367, -4.040999237037259384, 1.169951068917443049 ) ) ;
#14717=CARTESIAN_POINT ( 'NONE',  ( 29.21519671786122885, -8.552672223064927692, 2.713652344655544724 ) ) ;
#14729=CARTESIAN_POINT ( 'NONE',  ( 84.96607275259252390, -4.067036972963657071, -4.006106264892282276 ) ) ;
#14730=ORIENTED_EDGE ( 'NONE', *, *, #17868, .F. ) ;
#14734=CARTESIAN_POINT ( 'NONE',  ( 47.99002579008096347, -3.080023785605708220, 1.915219082070892531 ) ) ;
#14751=( BOUNDED_SURFACE ( )  B_SPLINE_SURFACE ( 3, 3, ( 
 ( #27612, #15057, #2391, #19598, #4206, #4714, #17060, #14883 ),
 ( #27458, #12218, #12563, #28610, #30952, #3197, #20753, #13206 ),
 ( #28260, #15555, #8033, #513, #17743, #18233, #20255, #18069 ),
 ( #10209, #20432, #15234, #3052, #22917, #5369, #28446, #15739 ) ),
 .UNSPECIFIED., .F., .F., .F. ) 
 B_SPLINE_SURFACE_WITH_KNOTS ( ( 4, 4 ),
 ( 4, 2, 2, 4 ),
 ( 0.000000000000000000, 1.000000000000000000 ),
 ( 0.000000000000000000, 0.5000000000000000000, 0.7500000000000000000, 1.000000000000000000 ),
 .UNSPECIFIED. ) 
 GEOMETRIC_REPRESENTATION_ITEM ( )  RATIONAL_B_SPLINE_SURFACE ( (
 ( 1.000000000000000000, 1.000000000000000000, 1.000000000000000000, 1.000000000000000000, 1.000000000000000000, 1.000000000000000000, 1.000000000000000000, 1.000000000000000000),
 ( 0.9743068154145675397, 0.9743068154145675397, 0.9743068154145675397, 0.9743068154145675397, 0.9743068154145675397, 0.9743068154145675397, 0.9743068154145675397, 0.9743068154145675397),
 ( 0.9743068154145675397, 0.9743068154145675397, 0.9743068154145675397, 0.9743068154145675397, 0.9743068154145675397, 0.9743068154145675397, 0.9743068154145675397, 0.9743068154145675397),
 ( 1.000000000000000000, 1.000000000000000000, 1.000000000000000000, 1.000000000000000000, 1.000000000000000000, 1.000000000000000000, 1.000000000000000000, 1.000000000000000000) ) ) 
 REPRESENTATION_ITEM ( '' )  SURFACE ( )  );
#14772=CARTESIAN_POINT ( 'NONE',  ( 47.88685968122761238, -4.079890078783551921, -1.529339664923148323 ) ) ;
#14784=FACE_BOUND ( 'NONE', #29541, .T. ) ;
#14786=CARTESIAN_POINT ( 'NONE',  ( 29.27523314209665983, -3.695744416148424527, -0.02339150518254430253 ) ) ;
#14787=EDGE_CURVE ( 'NONE', #15872, #25625, #1934, .T. ) ;
#14796=CARTESIAN_POINT ( 'NONE',  ( 0.000000000000000000, 0.000000000000000000, 0.000000000000000000 ) ) ;
#14802=CARTESIAN_POINT ( 'NONE',  ( 28.69360035300382705, -5.615748452717688188, 3.993434336046830513 ) ) ;
#14810=CARTESIAN_POINT ( 'NONE',  ( 101.7539407721759801, -3.355291987352425842, 4.312036717242840211 ) ) ;
#14827=CARTESIAN_POINT ( 'NONE',  ( 85.33608266635167183, -5.304379108986591262, -5.695980980372493008 ) ) ;
#14828=CARTESIAN_POINT ( 'NONE',  ( 29.21519671786122885, -8.552672223070194590, -2.713652344655543391 ) ) ;
#14835=CARTESIAN_POINT ( 'NONE',  ( 54.97676626710897096, -6.490013410911064540, 4.018750264949940032 ) ) ;
#14850=CARTESIAN_POINT ( 'NONE',  ( 23.71121667297774138, -6.322215142808039090, -3.993434336039487498 ) ) ;
#14861=DIRECTION ( 'NONE',  ( 0.000000000000000000, 0.000000000000000000, 1.000000000000000000 ) ) ;
#14879=CARTESIAN_POINT ( 'NONE',  ( 102.3451239296545623, -2.871394787408288796, -4.018750258909830286 ) ) ;
#14883=CARTESIAN_POINT ( 'NONE',  ( 18.58227844715246135, -7.846511338401735536, -2.713652344655542059 ) ) ;
#14918=VERTEX_POINT ( 'NONE', #3903 ) ;
#14936=DIRECTION ( 'NONE',  ( -0.08910563629484158366, -0.9960221812693186294, 0.000000000000000000 ) ) ;
#14939=CARTESIAN_POINT ( 'NONE',  ( 47.68482864957696421, -3.825617316378856714, -0.07017451552781628354 ) ) ;
#14962=CARTESIAN_POINT ( 'NONE',  ( 85.01592635901995720, -4.880223576643683892, -4.275175582424107112 ) ) ;
#14999=CARTESIAN_POINT ( 'NONE',  ( 18.75885765836901342, -5.872710146263817599, 4.003574682309002597 ) ) ;
#15029=CARTESIAN_POINT ( 'NONE',  ( 54.94526044242307705, -5.359369332727369262, 3.993434333344287435 ) ) ;
#15034=CARTESIAN_POINT ( 'NONE',  ( 48.08400536259535585, -8.675012021211058411, 2.713652344655544724 ) ) ;
#15036=CARTESIAN_POINT ( 'NONE',  ( 68.59913483175155591, -3.860138077755596697, 2.184958020780332522 ) ) ;
#15043=AXIS2_PLACEMENT_3D ( 'NONE', #26842, #19146, #3960 ) ;
#15048=CARTESIAN_POINT ( 'NONE',  ( 40.87792176339704042, -5.783270549457658838, -4.043900193582110170 ) ) ;
#15057=CARTESIAN_POINT ( 'NONE',  ( 85.45070076415389337, -7.158483446636732417, -2.713652344655542059 ) ) ;
#15075=AXIS2_PLACEMENT_3D ( 'NONE', #13746, #31988, #9057 ) ;
#15076=CARTESIAN_POINT ( 'NONE',  ( 18.74147553047095727, -6.067007450452971185, -3.690577026541935091 ) ) ;
#15114=CARTESIAN_POINT ( 'NONE',  ( 29.35001421184127324, -4.582605737176272953, -4.522129901861162260 ) ) ;
#15125=CARTESIAN_POINT ( 'NONE',  ( 19.01480233880806381, -3.011762293215138886, 0.07017451550800274385 ) ) ;
#15145=CARTESIAN_POINT ( 'NONE',  ( 54.77277180716814087, -8.244003004416214253, 0.07017451552781736601 ) ) ;
#15191=CARTESIAN_POINT ( 'NONE',  ( 28.66461310467470724, -6.745212029000279053, 4.023790193031063112 ) ) ;
#15206=CARTESIAN_POINT ( 'NONE',  ( 47.93076651534932608, -6.701564465775193824, -3.993434086979319453 ) ) ;
#15228=CARTESIAN_POINT ( 'NONE',  ( 18.85982315263666464, -4.744118555706133833, -4.006107076250019716 ) ) ;
#15234=CARTESIAN_POINT ( 'NONE',  ( 69.42401195566041849, -8.835509274224046194, -0.07017451552783579571 ) ) ;
#15243=DIRECTION ( 'NONE',  ( -0.9975973382524638833, -0.06927878976713691683, 0.000000000000000000 ) ) ;
#15264=ORIENTED_EDGE ( 'NONE', *, *, #4261, .F. ) ;
#15265=CARTESIAN_POINT ( 'NONE',  ( 23.61632761762314203, -8.296864917633476111, 2.713652344655544724 ) ) ;
#15278=CARTESIAN_POINT ( 'NONE',  ( 69.18703749905368738, -4.112663945013685485, -4.522129901861162260 ) ) ;
#15284=EDGE_CURVE ( 'NONE', #24285, #20638, #32212, .T. ) ;
#15288=CARTESIAN_POINT ( 'NONE',  ( 47.68482864957696421, -3.825617316378856714, 0.07017451550799964910 ) ) ;
#15289=CARTESIAN_POINT ( 'NONE',  ( 85.20563808598728883, -3.194259795296060300, 4.522129901861162260 ) ) ;
#15296=CARTESIAN_POINT ( 'NONE',  ( 101.9216173105994443, -5.769792427975428240, -0.07017451552783622593 ) ) ;
#15310=CARTESIAN_POINT ( 'NONE',  ( 41.45057005843676734, -9.239282957736858037, 1.915219082070893863 ) ) ;
#15317=CARTESIAN_POINT ( 'NONE',  ( 48.06508596181272708, -7.548662730762578654, 4.522129901861162260 ) ) ;
#15342=CARTESIAN_POINT ( 'NONE',  ( 40.88376184144740222, -6.854209834395733836, 4.053847216738481585 ) ) ;
#15360=VERTEX_POINT ( 'NONE', #24552 ) ;
#15364=CARTESIAN_POINT ( 'NONE',  ( 28.69355067553088645, -5.615744008485835437, 3.993434336029700216 ) ) ;
#15370=CARTESIAN_POINT ( 'NONE',  ( 101.6441386174529953, -1.774168274679931212, 2.184956718805492581 ) ) ;
#15372=CARTESIAN_POINT ( 'NONE',  ( 101.8797206818349821, -5.166491396337139719, -2.184956718990371805 ) ) ;
#15377=CARTESIAN_POINT ( 'NONE',  ( 40.87776742365452520, -5.755143957976294189, -4.003574183526315444 ) ) ;
#15393=CARTESIAN_POINT ( 'NONE',  ( 18.60867489490414428, -7.551452029063769444, -0.8134928201658568891 ) ) ;
#15409=CARTESIAN_POINT ( 'NONE',  ( 29.18953645666585217, -9.308308156628569918, 0.07017451552781736601 ) ) ;
#15434=CARTESIAN_POINT ( 'NONE',  ( 18.65791233782558933, -7.001076235494291033, 2.184956778801695254 ) ) ;
#15437=CARTESIAN_POINT ( 'NONE',  ( 23.58234648083524121, -8.048792613698569909, -0.07017451552783579571 ) ) ;
#15442=CARTESIAN_POINT ( 'NONE',  ( 19.03654924710325602, -2.768675503676416572, 2.713652344655542503 ) ) ;
#15450=CARTESIAN_POINT ( 'NONE',  ( 41.43141396789281572, -2.886852813804338780, -0.07017451552781628354 ) ) ;
#15457=CARTESIAN_POINT ( 'NONE',  ( 35.16139127360178662, -8.400504373793673096, 0.07017451552781736601 ) ) ;
#15472=VERTEX_POINT ( 'NONE', #28231 ) ;
#15499=CARTESIAN_POINT ( 'NONE',  ( 69.06945446451673831, -6.096442945251244971, 4.023790688806045956 ) ) ;
#15536=CARTESIAN_POINT ( 'NONE',  ( 55.01832146648882116, -7.980226898950165904, 1.529339875099998913 ) ) ;
#15542=CARTESIAN_POINT ( 'NONE',  ( 40.73830215457859794, -6.894995700253241822, -3.993433058221939724 ) ) ;
#15547=CARTESIAN_POINT ( 'NONE',  ( 18.84046687333923131, -4.960482910681117907, -4.215290389445589092 ) ) ;
#15555=CARTESIAN_POINT ( 'NONE',  ( 85.49734435724779757, -7.913007294147515580, -1.010822989962099960 ) ) ;
#15583=EDGE_CURVE ( 'NONE', #2205, #15872, #22221, .T. ) ;
#15621=CARTESIAN_POINT ( 'NONE',  ( 41.35536016469701082, -7.892720495295837857, 2.184957211607506000 ) ) ;
#15627=CARTESIAN_POINT ( 'NONE',  ( 48.05280571049737404, -6.817569152029394175, 5.695980980372492120 ) ) ;
#15639=CARTESIAN_POINT ( 'NONE',  ( 47.98568197278775216, -2.821418575600922019, -0.07017451552781628354 ) ) ;
#15644=CARTESIAN_POINT ( 'NONE',  ( 29.41391112839824373, -2.700987858903443950, -0.07017451552781585333 ) ) ;
#15648=ORIENTED_EDGE ( 'NONE', *, *, #22134, .T. ) ;
#15651=ORIENTED_EDGE ( 'NONE', *, *, #20020, .F. ) ;
#15655=CARTESIAN_POINT ( 'NONE',  ( 18.53796472816966912, -8.341849780241114232, 1.915219082070893863 ) ) ;
#15688=CARTESIAN_POINT ( 'NONE',  ( 19.03654924710325602, -2.768675503676416572, -2.713652344655543391 ) ) ;
#15691=CARTESIAN_POINT ( 'NONE',  ( 18.76345385348679429, -5.821333909315332455, 4.073741754928252412 ) ) ;
#15708=CARTESIAN_POINT ( 'NONE',  ( 85.05927807847527333, -5.579234875939544480, -3.390607678631389010 ) ) ;
#15710=ORIENTED_EDGE ( 'NONE', *, *, #24873, .F. ) ;
#15718=CARTESIAN_POINT ( 'NONE',  ( 68.56906952848774495, -3.255983411058744004, -0.07017451552781628354 ) ) ;
#15721=CARTESIAN_POINT ( 'NONE',  ( 29.18336473368350070, -8.306880066003914820, 0.07017451552781851787 ) ) ;
#15732=CARTESIAN_POINT ( 'NONE',  ( 84.96912909400775504, -4.116878033481301102, -4.073740955716186996 ) ) ;
#15738=B_SPLINE_CURVE_WITH_KNOTS ( 'NONE', 3,
 ( #31898, #26548, #21540, #16662, #4295, #1625, #9309, #13978, #8965, #19356 ),
 .UNSPECIFIED., .F., .F.,
 ( 4, 3, 3, 4 ),
 ( 0.000000000000000000, 0.0005352572989639539907, 0.001070514597927907331, 0.002130599681840938692 ),
 .UNSPECIFIED. ) ;
#15739=CARTESIAN_POINT ( 'NONE',  ( 18.51491971917342028, -8.599446730134173933, -0.07017451552783579571 ) ) ;
#15786=CARTESIAN_POINT ( 'NONE',  ( 19.03654924710324892, -2.768675503676413019, -2.713652344655541615 ) ) ;
#15804=CARTESIAN_POINT ( 'NONE',  ( 23.95058674323864523, -2.449331254355788356, -1.010822989962086416 ) ) ;
#15807=ORIENTED_EDGE ( 'NONE', *, *, #19612, .T. ) ;
#15814=CARTESIAN_POINT ( 'NONE',  ( 85.45070076415389337, -7.158483446636730640, 2.713652344655544724 ) ) ;
#15824=CARTESIAN_POINT ( 'NONE',  ( 35.27668332986648636, -7.991339570346063681, -1.873789188797430727 ) ) ;
#15841=CARTESIAN_POINT ( 'NONE',  ( 102.4203624159291195, -3.957500511122341358, 4.053847705490468911 ) ) ;
#15853=B_SPLINE_SURFACE_WITH_KNOTS ( 'NONE', 1, 3, ( 
 ( #6069, #25980, #23786, #21129, #31327, #8886, #5884, #16074 ),
 ( #26131, #6220, #898, #26305, #8552, #11075, #8405, #3415 ) ),
 .UNSPECIFIED., .F., .F., .F.,
 ( 2, 2 ),
 ( 4, 2, 2, 4 ),
 ( 0.000000000000000000, 1.000000000000000000 ),
 ( 0.000000000000000000, 0.5000000000000000000, 0.7500000000000000000, 1.000000000000000000 ),
 .UNSPECIFIED. ) ;
#15860=CARTESIAN_POINT ( 'NONE',  ( 85.20563808598728883, -3.194259795296060300, 4.522129901861162260 ) ) ;
#15862=CARTESIAN_POINT ( 'NONE',  ( 23.84714171513401126, -3.444070612163515843, -0.07017451552781626967 ) ) ;
#15864=CARTESIAN_POINT ( 'NONE',  ( 85.14283307489681363, -6.932413485865820846, 0.4367664097854566663 ) ) ;
#15871=CARTESIAN_POINT ( 'NONE',  ( 101.8933637717057223, -5.362948496501876328, -1.868788700206728048 ) ) ;
#15872=VERTEX_POINT ( 'NONE', #7303 ) ;
#15876=CARTESIAN_POINT ( 'NONE',  ( 18.85537384076560841, -4.793852932768607467, -4.073741754935396919 ) ) ;
#15880=EDGE_CURVE ( 'NONE', #18631, #19567, #25424, .T. ) ;
#15896=CARTESIAN_POINT ( 'NONE',  ( 101.7619443659971950, -3.470541747333645954, 3.636029349014984202 ) ) ;
#15947=CARTESIAN_POINT ( 'NONE',  ( 41.43219399711119877, -3.145521524155372006, -1.915219082070890755 ) ) ;
#15956=CARTESIAN_POINT ( 'NONE',  ( 29.33517104213873239, -3.852857368063288046, -1.169950485888521463 ) ) ;
#15958=CARTESIAN_POINT ( 'NONE',  ( 85.49734435724778336, -7.913007294147514692, 0.07017451552781803215 ) ) ;
#15965=CARTESIAN_POINT ( 'NONE',  ( 18.62691943105446057, -7.347514731314632286, -1.529339877378613100 ) ) ;
#15981=CARTESIAN_POINT ( 'NONE',  ( 40.87760899951555160, -5.748707280016356336, -3.993433839269025842 ) ) ;
#15988=CARTESIAN_POINT ( 'NONE',  ( 102.3526732589231898, -2.980372452608875733, 4.155404932455299516 ) ) ;
#16020=CARTESIAN_POINT ( 'NONE',  ( 101.9038547928002316, -5.514016590425875997, -1.527295561052322892 ) ) ;
#16074=CARTESIAN_POINT ( 'NONE',  ( 18.68265047573912341, -6.724553502642427461, -4.522129901861164036 ) ) ;
#16091=CARTESIAN_POINT ( 'NONE',  ( 23.64679384717597443, -7.447389048103699061, 2.184956778805557498 ) ) ;
#16096=CARTESIAN_POINT ( 'NONE',  ( 41.19430503359222939, -3.886431767407559246, 0.07017451552849453267 ) ) ;
#16106=VECTOR ( 'NONE', #30259, 1000.000000000000000 ) ;
#16112=ORIENTED_EDGE ( 'NONE', *, *, #14787, .T. ) ;
#16128=CARTESIAN_POINT ( 'NONE',  ( 23.87614828266624301, -3.446665583135119171, -0.07017451552781975299 ) ) ;
#16161=CARTESIAN_POINT ( 'NONE',  ( 28.70307564580845749, -5.239617037334318717, -3.390608483621579516 ) ) ;
#16166=CARTESIAN_POINT ( 'NONE',  ( 18.85603800621453630, -4.786428896025966218, 4.074610069492402786 ) ) ;
#16186=CARTESIAN_POINT ( 'NONE',  ( 47.94941403272093083, -7.827919050457508909, -2.184956529774258804 ) ) ;
#16196=CARTESIAN_POINT ( 'NONE',  ( 18.93617721851659041, -3.890633339435721982, 4.522129901861162260 ) ) ;
#16241=CARTESIAN_POINT ( 'NONE',  ( 101.8538325601235783, -4.793708883847108915, -2.784893846770871040 ) ) ;
#16249=CARTESIAN_POINT ( 'NONE',  ( 84.65816297383780409, -6.961284151106491791, -0.07017451552783603164 ) ) ;
#16260=CARTESIAN_POINT ( 'NONE',  ( 102.6421141555943706, -1.710335469228581484, -0.07017451552783579571 ) ) ;
#16307=B_SPLINE_CURVE_WITH_KNOTS ( 'NONE', 3,
 ( #13276, #31695, #23482, #8290, #18484, #5773 ),
 .UNSPECIFIED., .F., .F.,
 ( 4, 2, 4 ),
 ( 0.009541643435016143593, 0.5047708217175082002, 1.000000000000000000 ),
 .UNSPECIFIED. ) ;
#16309=CARTESIAN_POINT ( 'NONE',  ( 41.35712849199997265, -8.497574858407940468, -0.4367667074098299795 ) ) ;
#16316=CARTESIAN_POINT ( 'NONE',  ( 18.51491971917340607, -8.599446730134173933, 0.07017451552781736601 ) ) ;
#16318=ORIENTED_EDGE ( 'NONE', *, *, #2209, .F. ) ;
#16326=CARTESIAN_POINT ( 'NONE',  ( 28.72212596679750263, -4.487363129039004583, -2.184956778818292200 ) ) ;
#16330=CARTESIAN_POINT ( 'NONE',  ( 40.88155443523169197, -6.447799953524727457, 4.312042181580753031 ) ) ;
#16341=ORIENTED_EDGE ( 'NONE', *, *, #30202, .T. ) ;
#16364=CARTESIAN_POINT ( 'NONE',  ( 40.88398291294785025, -6.895006614273913925, 3.995970210903281750 ) ) ;
#16404=CARTESIAN_POINT ( 'NONE',  ( 102.3440491116951563, -2.855879258563742251, -3.995006639038339191 ) ) ;
#16445=CARTESIAN_POINT ( 'NONE',  ( 102.2233072702345282, -1.127920370132907024, -0.4367666012504502482 ) ) ;
#16453=CARTESIAN_POINT ( 'NONE',  ( 41.35698357845723905, -8.446179956401207889, -0.8105618903102438377 ) ) ;
#16477=CARTESIAN_POINT ( 'NONE',  ( 69.02444692756159839, -5.195103839446206351, 4.215290682826566382 ) ) ;
#16479=CARTESIAN_POINT ( 'NONE',  ( 28.68776846592777829, -5.841437261377540047, -4.215290389454363407 ) ) ;
#16490=CARTESIAN_POINT ( 'NONE',  ( 18.51491971917340607, -8.599446730134173933, -0.07017451552781736601 ) ) ;
#16513=CARTESIAN_POINT ( 'NONE',  ( 28.66414223207782896, -6.763717812351308645, 3.995970707797161570 ) ) ;
#16535=ORIENTED_EDGE ( 'NONE', *, *, #9825, .F. ) ;
#16560=CARTESIAN_POINT ( 'NONE',  ( 84.96565083440447097, -4.060156691890333569, -3.995335864730365394 ) ) ;
#16602=B_SPLINE_CURVE_WITH_KNOTS ( 'NONE', 3,
 ( #12495, #12154, #22352, #12648, #10126, #20350, #7648, #10804 ),
 .UNSPECIFIED., .F., .F.,
 ( 4, 2, 2, 4 ),
 ( 0.000000000000000000, 0.5000000000000000000, 0.7500000000000000000, 1.000000000000000000 ),
 .UNSPECIFIED. ) ;
#16613=EDGE_LOOP ( 'NONE', ( #24742, #13881, #7209, #23325 ) ) ;
#16625=CARTESIAN_POINT ( 'NONE',  ( 85.14283307489681363, -6.932413485865820846, -0.4367664097874476292 ) ) ;
#16652=CARTESIAN_POINT ( 'NONE',  ( 102.3439814245663655, -2.854902261462827884, 3.993434327364640435 ) ) ;
#16656=CARTESIAN_POINT ( 'NONE',  ( 54.94707873175313750, -5.417356489197679537, -4.073741752274519179 ) ) ;
#16662=CARTESIAN_POINT ( 'NONE',  ( 18.93569951633547177, -3.895973091535266608, -2.639289341045732762 ) ) ;
#16684=CIRCLE ( 'NONE', #25244, 1.676012832569465205 ) ;
#16686=B_SPLINE_CURVE_WITH_KNOTS ( 'NONE', 3,
 ( #15372, #15871, #16020, #17908, #26081, #205 ),
 .UNSPECIFIED., .F., .F.,
 ( 4, 2, 4 ),
 ( 0.000000000000000000, 0.001111101124723993692, 0.002222202249447986951 ),
 .UNSPECIFIED. ) ;
#16689=FACE_OUTER_BOUND ( 'NONE', #68, .T. ) ;
#16699=CARTESIAN_POINT ( 'NONE',  ( 28.66412195420384634, -6.764514867728558478, 3.994702635811785196 ) ) ;
#16737=CARTESIAN_POINT ( 'NONE',  ( 54.90142980599745925, -3.782945109527762639, 1.169950777188785596 ) ) ;
#16743=CARTESIAN_POINT ( 'NONE',  ( 47.99837860531645362, -3.577301031427907230, -2.713652344655542503 ) ) ;
#16752=CARTESIAN_POINT ( 'NONE',  ( 40.87774960799753643, -5.751897813703351403, -3.998505783863144813 ) ) ;
#16772=CARTESIAN_POINT ( 'NONE',  ( 54.97742507208633356, -6.506533559248902421, 3.993434333358794053 ) ) ;
#16774=CARTESIAN_POINT ( 'NONE',  ( 102.8580990270160385, -4.820463887425400884, -4.522129901861164036 ) ) ;
#16793=ORIENTED_EDGE ( 'NONE', *, *, #4260, .F. ) ;
#16800=CARTESIAN_POINT ( 'NONE',  ( 41.34457103394125710, -4.143788916011438950, -1.529340246550954685 ) ) ;
#16801=EDGE_LOOP ( 'NONE', ( #20258, #3451, #4650, #9071 ) ) ;
#16865=CARTESIAN_POINT ( 'NONE',  ( 54.97719654313131343, -6.505560170230147321, 3.995006645005578338 ) ) ;
#16896=( BOUNDED_SURFACE ( )  B_SPLINE_SURFACE ( 3, 3, ( 
 ( #18136, #5448, #5626, #7946, #25666, #15644, #12964, #289 ),
 ( #23329, #13127, #20512, #433, #18319, #17989, #15804, #28675 ),
 ( #10613, #26012, #23480, #5771, #15947, #3272, #13436, #26643 ),
 ( #26987, #29314, #1569, #19123, #11596, #21303, #3751, #13918 ) ),
 .UNSPECIFIED., .F., .F., .F. ) 
 B_SPLINE_SURFACE_WITH_KNOTS ( ( 4, 4 ),
 ( 4, 2, 2, 4 ),
 ( 0.000000000000000000, 1.000000000000000000 ),
 ( 0.000000000000000000, 0.5000000000000000000, 0.7500000000000000000, 1.000000000000000000 ),
 .UNSPECIFIED. ) 
 GEOMETRIC_REPRESENTATION_ITEM ( )  RATIONAL_B_SPLINE_SURFACE ( (
 ( 1.000000000000000000, 1.000000000000000000, 1.000000000000000000, 1.000000000000000000, 1.000000000000000000, 1.000000000000000000, 1.000000000000000000, 1.000000000000000000),
 ( 0.9743068154145673176, 0.9743068154145673176, 0.9743068154145673176, 0.9743068154145673176, 0.9743068154145673176, 0.9743068154145673176, 0.9743068154145673176, 0.9743068154145673176),
 ( 0.9743068154145673176, 0.9743068154145673176, 0.9743068154145673176, 0.9743068154145673176, 0.9743068154145673176, 0.9743068154145673176, 0.9743068154145673176, 0.9743068154145673176),
 ( 1.000000000000000000, 1.000000000000000000, 1.000000000000000000, 1.000000000000000000, 1.000000000000000000, 1.000000000000000000, 1.000000000000000000, 1.000000000000000000) ) ) 
 REPRESENTATION_ITEM ( '' )  SURFACE ( )  );
#16907=CARTESIAN_POINT ( 'NONE',  ( 69.01333418885296567, -4.972402945391593221, -3.997239029220839068 ) ) ;
#16981=CARTESIAN_POINT ( 'NONE',  ( 85.02201553618581897, -4.979580722663584424, -4.215289907568986472 ) ) ;
#17008=CARTESIAN_POINT ( 'NONE',  ( 23.63572006014529592, -7.640988024200195738, 1.873789191059426429 ) ) ;
#17013=CARTESIAN_POINT ( 'NONE',  ( 85.03530313761559967, -5.196410162969478996, 4.006106264926406979 ) ) ;
#17039=CARTESIAN_POINT ( 'NONE',  ( 68.94677942531217241, -3.651108094209274846, 1.873789666860799619 ) ) ;
#17042=CARTESIAN_POINT ( 'NONE',  ( 101.6829671662719790, -2.333289718345304298, 3.084778200030451334 ) ) ;
#17056=CARTESIAN_POINT ( 'NONE',  ( 40.87774081726615094, -5.750296118533150924, -3.995970210918201815 ) ) ;
#17060=CARTESIAN_POINT ( 'NONE',  ( 23.61632761765384458, -8.296864917636222359, -2.713652344655542059 ) ) ;
#17108=CARTESIAN_POINT ( 'NONE',  ( 54.90853374639801388, -4.039626021003738465, -1.873789188464666466 ) ) ;
#17112=LINE ( 'NONE', #22309, #18143 ) ;
#17128=CARTESIAN_POINT ( 'NONE',  ( 41.44567272411835290, -7.615257740949710197, 4.522129901861163148 ) ) ;
#17141=CARTESIAN_POINT ( 'NONE',  ( 101.7460807238309570, -3.242109246518175336, -4.282234000298882570 ) ) ;
#17152=CARTESIAN_POINT ( 'NONE',  ( 40.88155443526453325, -6.447799953488541291, -4.312042181587000478 ) ) ;
#17184=CARTESIAN_POINT ( 'NONE',  ( 29.32519546910713970, -5.313460878238872809, -5.695980980372493008 ) ) ;
#17196=CARTESIAN_POINT ( 'NONE',  ( 28.66416261876312532, -6.762916490609137021, 3.997238537448035700 ) ) ;
#17233=B_SPLINE_SURFACE_WITH_KNOTS ( 'NONE', 3, 3, ( 
 ( #322, #8320, #23851, #8630, #10993, #16326, #816 ),
 ( #3007, #18517, #28710, #21194, #13647, #30908, #31392 ),
 ( #31247, #26047, #23361, #468, #28378, #16161, #13160 ),
 ( #8467, #18664, #3491, #13007, #15981, #29052, #28863 ) ),
 .UNSPECIFIED., .F., .F., .F.,
 ( 4, 4 ),
 ( 4, 3, 4 ),
 ( -7.601402592587692883E-13, 1.000000000000000444 ),
 ( 0.003594141869012155120, 0.5017970709346459834, 1.000000000000279776 ),
 .UNSPECIFIED. ) ;
#17236=CARTESIAN_POINT ( 'NONE',  ( 102.2339617642406182, -1.281710854345167849, 1.169950773171794633 ) ) ;
#17246=EDGE_LOOP ( 'NONE', ( #1573, #8113, #1628, #15648 ) ) ;
#17251=CARTESIAN_POINT ( 'NONE',  ( 69.01403922547133618, -4.986533802114832881, -4.018750763356134570 ) ) ;
#17257=CARTESIAN_POINT ( 'NONE',  ( 41.43369393131070666, -3.642920876114435824, 2.713652344655541615 ) ) ;
#17301=CARTESIAN_POINT ( 'NONE',  ( 23.85260150830463033, -3.857138523344298076, -1.873789191062679160 ) ) ;
#17308=AXIS2_PLACEMENT_3D ( 'NONE', #15896, #15243, #22926 ) ;
#17314=CARTESIAN_POINT ( 'NONE',  ( 41.20585001718148277, -8.497180311781159290, -0.02339150517595086839 ) ) ;
#17316=CARTESIAN_POINT ( 'NONE',  ( 35.23476908784419237, -3.791088091780328906, -0.07017451552781628354 ) ) ;
#17348=CARTESIAN_POINT ( 'NONE',  ( 29.41391112839825794, -2.700987858898180161, -0.07017451552781628354 ) ) ;
#17352=EDGE_CURVE ( 'NONE', #5699, #6454, #1442, .T. ) ;
#17363=CARTESIAN_POINT ( 'NONE',  ( 41.43709133142961321, -4.769546740945156849, -4.522129901861162260 ) ) ;
#17367=CARTESIAN_POINT ( 'NONE',  ( 18.99195638486427384, -3.267134207175613536, 1.527295581757372123 ) ) ;
#17372=CARTESIAN_POINT ( 'NONE',  ( 40.88393865713020858, -6.886838077535163194, 4.008636882558729297 ) ) ;
#17387=CARTESIAN_POINT ( 'NONE',  ( 35.29731606331278471, -6.671246578258721804, -3.993434333679743986 ) ) ;
#17388=ORIENTED_EDGE ( 'NONE', *, *, #6524, .T. ) ;
#17399=CARTESIAN_POINT ( 'NONE',  ( 102.2651039925859209, -1.731228206879544373, 2.184956770111046165 ) ) ;
#17400=FACE_OUTER_BOUND ( 'NONE', #6068, .T. ) ;
#17412=CARTESIAN_POINT ( 'NONE',  ( 84.96658996055005275, -4.075471198594033062, -4.018749453393667181 ) ) ;
#17416=FACE_OUTER_BOUND ( 'NONE', #18059, .T. ) ;
#17441=CARTESIAN_POINT ( 'NONE',  ( 18.93617721851659041, -3.890633339435721982, 4.522129901861162260 ) ) ;
#17452=VERTEX_POINT ( 'NONE', #33021 ) ;
#17460=CARTESIAN_POINT ( 'NONE',  ( 35.16139127360178662, -8.400504373793673096, 0.02339150517593243869 ) ) ;
#17462=CARTESIAN_POINT ( 'NONE',  ( 35.23476908784419237, -3.791088091780328906, -0.02339150518254430253 ) ) ;
#17494=CARTESIAN_POINT ( 'NONE',  ( 29.25343337322282622, -7.426690278353109242, 4.522129901861162260 ) ) ;
#17496=CARTESIAN_POINT ( 'NONE',  ( 101.6833487790503341, -2.338784847420880553, -3.093621779973272812 ) ) ;
#17502=B_SPLINE_CURVE_WITH_KNOTS ( 'NONE', 3,
 ( #8858, #26587, #19066, #13210, #518, #29920 ),
 .UNSPECIFIED., .F., .F.,
 ( 4, 2, 4 ),
 ( 0.009527197497169513293, 0.5047635987485847853, 1.000000000000000000 ),
 .UNSPECIFIED. ) ;
#17518=CARTESIAN_POINT ( 'NONE',  ( 69.07021576803677476, -6.111680664911116168, 4.001041175462015431 ) ) ;
#17519=CARTESIAN_POINT ( 'NONE',  ( 19.01480233880980819, -3.011762293215293429, -0.07017451552781921176 ) ) ;
#17558=CARTESIAN_POINT ( 'NONE',  ( 40.87782285394631998, -5.765244507547243380, -4.018749766559461811 ) ) ;
#17563=CARTESIAN_POINT ( 'NONE',  ( 19.10390797508229710, -2.015740111943975066, 0.07017451552782173751 ) ) ;
#17577=CARTESIAN_POINT ( 'NONE',  ( 18.74987994845499628, -5.973062925086321862, -3.842005681288779950 ) ) ;
#17589=APPLICATION_CONTEXT ( 'configuration controlled 3d designs of mechanical parts and assemblies' ) ;
#17618=CARTESIAN_POINT ( 'NONE',  ( 68.79832465278998654, -7.861404707920828905, 0.02339150517593243869 ) ) ;
#17620=CARTESIAN_POINT ( 'NONE',  ( 29.27523314209665628, -3.695744416148424971, 0.07017451550799837234 ) ) ;
#17650=CARTESIAN_POINT ( 'NONE',  ( 101.7777785755449855, -3.698550425766125471, 4.282234000388568163 ) ) ;
#17683=CARTESIAN_POINT ( 'NONE',  ( 69.06963061213430422, -6.099968625253806565, 4.018750763354483446 ) ) ;
#17719=CARTESIAN_POINT ( 'NONE',  ( 19.01480233880637982, -3.011762293214985675, 0.4367666033482894283 ) ) ;
#17729=VECTOR ( 'NONE', #26841, 1000.000000000000114 ) ;
#17734=CARTESIAN_POINT ( 'NONE',  ( 69.01532733225560889, -5.012350318234797264, -4.053848206251212005 ) ) ;
#17743=CARTESIAN_POINT ( 'NONE',  ( 41.45135008765517881, -9.497951668093163491, -1.010822989962099960 ) ) ;
#17747=CARTESIAN_POINT ( 'NONE',  ( 102.6609843814833027, -1.982062027707615526, -4.522129901861162260 ) ) ;
#17799=CARTESIAN_POINT ( 'NONE',  ( 101.6200045064549329, -1.426643080118511708, 1.527295561047710803 ) ) ;
#17822=CARTESIAN_POINT ( 'NONE',  ( 18.75828436641558028, -5.879118399717574661, -3.993434336035625254 ) ) ;
#17830=ORIENTED_EDGE ( 'NONE', *, *, #24650, .T. ) ;
#17868=EDGE_CURVE ( 'NONE', #32072, #15472, #20011, .T. ) ;
#17874=CARTESIAN_POINT ( 'NONE',  ( 69.06834080223671890, -6.074152155849746215, 4.053848206249033304 ) ) ;
#17875=CARTESIAN_POINT ( 'NONE',  ( 19.01480233880980464, -3.011762293215291653, -0.4426577274541297347 ) ) ;
#17902=CARTESIAN_POINT ( 'NONE',  ( 29.34042402276601891, -3.698761498129244263, 0.07017451552756237554 ) ) ;
#17903=CARTESIAN_POINT ( 'NONE',  ( 41.44907012423725234, -8.741883605793594469, 2.713652344655544724 ) ) ;
#17908=CARTESIAN_POINT ( 'NONE',  ( 101.9180023365599936, -5.717737701100571890, -0.8134928171553283960 ) ) ;
#17913=CARTESIAN_POINT ( 'NONE',  ( 102.3463693925194917, -2.889373554450824333, -4.043900685077098878 ) ) ;
#17919=CARTESIAN_POINT ( 'NONE',  ( 102.8769692529049564, -5.092190445904434704, 0.07017451552783667001 ) ) ;
#17949=CARTESIAN_POINT ( 'NONE',  ( 85.49734435724840864, -7.913007294147472059, 0.07017451552781736601 ) ) ;
#17951=CARTESIAN_POINT ( 'NONE',  ( 101.9216173105994443, -5.769792427975438009, 0.07017451552781736601 ) ) ;
#17970=CARTESIAN_POINT ( 'NONE',  ( 85.10546509784848013, -6.328795743774838556, 2.184955973835313703 ) ) ;
#17975=B_SPLINE_CURVE_WITH_KNOTS ( 'NONE', 3,
 ( #14360, #32462, #1693, #24260, #24761, #4193, #6536, #29778 ),
 .UNSPECIFIED., .F., .F.,
 ( 4, 2, 2, 4 ),
 ( 0.000000000000000000, 0.5000000000000000000, 0.7500000000000000000, 1.000000000000000000 ),
 .UNSPECIFIED. ) ;
#17989=CARTESIAN_POINT ( 'NONE',  ( 29.41391112839824373, -2.700987858898175276, -1.010822989962086416 ) ) ;
#17991=CARTESIAN_POINT ( 'NONE',  ( 101.9216173105994159, -5.769792427975438898, 0.07017451552781732438 ) ) ;
#18001=CARTESIAN_POINT ( 'NONE',  ( 102.9885081044300676, -6.698322160490905119, 1.010822989962089746 ) ) ;
#18008=CARTESIAN_POINT ( 'NONE',  ( 35.27266127981218347, -8.248087266145425644, -1.169950777424758170 ) ) ;
#18028=CARTESIAN_POINT ( 'NONE',  ( 85.03320566163840510, -5.162181109351803521, 4.053846905913455423 ) ) ;
#18054=CARTESIAN_POINT ( 'NONE',  ( 41.34386496145283729, -3.886814715717017865, 0.4367667078936094960 ) ) ;
#18055=CARTESIAN_POINT ( 'NONE',  ( 69.14445055419174935, -7.589252662750706868, 1.529340293463288480 ) ) ;
#18058=CARTESIAN_POINT ( 'NONE',  ( 18.93617721851659041, -3.890633339435721982, 4.522129901861162260 ) ) ;
#18059=EDGE_LOOP ( 'NONE', ( #26775, #6399, #26492, #31923 ) ) ;
#18063=CARTESIAN_POINT ( 'NONE',  ( 84.97936832876808921, -4.283865861974220479, -4.215289907538689818 ) ) ;
#18065=ORIENTED_EDGE ( 'NONE', *, *, #10569, .F. ) ;
#18069=CARTESIAN_POINT ( 'NONE',  ( 18.51491971917342028, -8.599446730134173933, -1.010822989962099960 ) ) ;
#18094=CARTESIAN_POINT ( 'NONE',  ( 48.09670199522223299, -9.430894477028838097, -0.07017451552783579571 ) ) ;
#18095=EDGE_CURVE ( 'NONE', #28727, #25625, #25196, .T. ) ;
#18125=CARTESIAN_POINT ( 'NONE',  ( 23.72239361536733782, -6.441344918542153408, 5.695980980372492120 ) ) ;
#18132=ORIENTED_EDGE ( 'NONE', *, *, #392, .F. ) ;
#18136=CARTESIAN_POINT ( 'NONE',  ( 102.5305753040692736, -0.1042037546421150512, -0.07017451552781585333 ) ) ;
#18143=VECTOR ( 'NONE', #30343, 1000.000000000000000 ) ;
#18147=CARTESIAN_POINT ( 'NONE',  ( 102.9885081044300676, -6.698322160490901567, 0.07017451552781803215 ) ) ;
#18178=CARTESIAN_POINT ( 'NONE',  ( 102.4167958684119668, -3.906015252786475322, 4.112224487556747299 ) ) ;
#18197=CARTESIAN_POINT ( 'NONE',  ( 23.66826818115595188, -7.072331084912446109, -2.787782631235886210 ) ) ;
#18210=CARTESIAN_POINT ( 'NONE',  ( 101.6022419886208610, -1.170867242066747860, -0.07017451552781628354 ) ) ;
#18213=CARTESIAN_POINT ( 'NONE',  ( 18.60402535544292490, -7.603424548862589560, 0.4367666033480746557 ) ) ;
#18224=CARTESIAN_POINT ( 'NONE',  ( 54.95446108375549699, -5.684089628123738080, -4.275175837990625283 ) ) ;
#18233=CARTESIAN_POINT ( 'NONE',  ( 29.18953645666586993, -9.308308156628571695, -1.010822989962099960 ) ) ;
#18252=CARTESIAN_POINT ( 'NONE',  ( 84.55169161418332635, -5.233307109668325907, 3.993432236216280629 ) ) ;
#18270=CIRCLE ( 'NONE', #23068, 5.000000000000000000 ) ;
#18286=CARTESIAN_POINT ( 'NONE',  ( 18.66631667619762780, -6.907132599765741787, 2.336383999542480439 ) ) ;
#18296=CARTESIAN_POINT ( 'NONE',  ( 55.00858942667073137, -7.632540988274553406, 2.184956776124872935 ) ) ;
#18304=CARTESIAN_POINT ( 'NONE',  ( 47.99837860531645362, -3.577301031424839017, 2.713652344655542503 ) ) ;
#18319=CARTESIAN_POINT ( 'NONE',  ( 41.43141396789279440, -2.886852813804333007, -1.010822989962086416 ) ) ;
#18342=CARTESIAN_POINT ( 'NONE',  ( 41.35597062191753537, -8.086568374296689399, -1.873789609314816307 ) ) ;
#18352=EDGE_CURVE ( 'NONE', #20638, #2621, #28417, .T. ) ;
#18367=DIRECTION ( 'NONE',  ( -0.04710975479914573244, -0.5265925107009691297, -0.8488115212910426477 ) ) ;
#18369=CARTESIAN_POINT ( 'NONE',  ( 69.06389083184971867, -5.985077526012525517, 4.150066331403145625 ) ) ;
#18377=CARTESIAN_POINT ( 'NONE',  ( 18.85511084203137955, -4.796792731031784385, 4.091315477141355572 ) ) ;
#18399=CARTESIAN_POINT ( 'NONE',  ( 35.27266127981243926, -8.248087266147095420, 1.169950777418872212 ) ) ;
#18406=CARTESIAN_POINT ( 'NONE',  ( 85.13613392229180477, -2.069934983084472879, 2.713652344655542503 ) ) ;
#18413=CARTESIAN_POINT ( 'NONE',  ( 40.87869491147504419, -5.924290355801652197, -4.185347298794283688 ) ) ;
#18459=CARTESIAN_POINT ( 'NONE',  ( 18.69152969128558084, -6.625301692630690908, 2.790665661679905707 ) ) ;
#18472=CARTESIAN_POINT ( 'NONE',  ( 29.32519546910717168, -5.313460878238876361, 5.695980980372492120 ) ) ;
#18480=CARTESIAN_POINT ( 'NONE',  ( 18.81968334181831892, -5.192801080986814810, -4.312047644171949301 ) ) ;
#18484=CARTESIAN_POINT ( 'NONE',  ( 28.66386174152028588, -4.482150724279978071, -2.184956778825816848 ) ) ;
#18490=CARTESIAN_POINT ( 'NONE',  ( 54.89716490669064797, -3.628845007888691132, -0.4367666026988534789 ) ) ;
#18499=CARTESIAN_POINT ( 'NONE',  ( 35.27427105688909847, -8.145327135406411401, -1.529339875379911229 ) ) ;
#18508=CARTESIAN_POINT ( 'NONE',  ( 28.72212596679959162, -4.487363129042812204, 2.184956778824082235 ) ) ;
#18517=CARTESIAN_POINT ( 'NONE',  ( 84.91897426281094852, -3.309433673474704296, -2.787781823995287844 ) ) ;
#18521=CARTESIAN_POINT ( 'NONE',  ( 28.66985322744079312, -6.539611658484044021, 4.215290389448495212 ) ) ;
#18535=ORIENTED_EDGE ( 'NONE', *, *, #29522, .T. ) ;
#18548=CARTESIAN_POINT ( 'NONE',  ( 47.95950916398558661, -8.432626694227655761, 0.4367665434690334303 ) ) ;
#18552=CARTESIAN_POINT ( 'NONE',  ( 41.43369393131070666, -3.642920876109168926, 2.713652344655542503 ) ) ;
#18553=ORIENTED_EDGE ( 'NONE', *, *, #3089, .T. ) ;
#18579=ADVANCED_FACE ( 'NONE', ( #17400 ), #8388, .T. ) ;
#18581=CARTESIAN_POINT ( 'NONE',  ( 18.72466669454978927, -6.254896501190466473, -3.387719717048244483 ) ) ;
#18589=CARTESIAN_POINT ( 'NONE',  ( 23.58234648083103124, -8.048792613723655620, -0.07017451552783530999 ) ) ;
#18601=DIRECTION ( 'NONE',  ( 0.06927878976713817971, -0.9975973382524637723, 0.000000000000000000 ) ) ;
#18631=VERTEX_POINT ( 'NONE', #10027 ) ;
#18647=CARTESIAN_POINT ( 'NONE',  ( 47.95695783165756154, -8.278479088712042966, -1.169950612933553513 ) ) ;
#18664=CARTESIAN_POINT ( 'NONE',  ( 84.96516786084956152, -4.058994088351913554, -3.993433528812653677 ) ) ;
#18669=CARTESIAN_POINT ( 'NONE',  ( 54.96481031288562491, -6.058022586631627959, 4.312042181580753031 ) ) ;
#18699=CARTESIAN_POINT ( 'NONE',  ( 55.02542983044660474, -8.237060396196270062, 0.07017451552781985014 ) ) ;
#18707=CARTESIAN_POINT ( 'NONE',  ( 18.75842578876440214, -5.877537581689508350, 3.995970707747694473 ) ) ;
#18737=CARTESIAN_POINT ( 'NONE',  ( 101.8147510725781473, -4.230945185443697909, -3.690576987646877249 ) ) ;
#18741=ADVANCED_FACE ( 'NONE', ( #26424 ), #31358, .F. ) ;
#18767=DIRECTION ( 'NONE',  ( -0.9975973382524639943, -0.06927878976713693071, 0.000000000000000000 ) ) ;
#18779=CARTESIAN_POINT ( 'NONE',  ( 23.68974245684579927, -6.697273116530260140, 3.390608483628176018 ) ) ;
#18817=CARTESIAN_POINT ( 'NONE',  ( 84.87411226253082930, -2.587501188392339113, -1.529339190611058052 ) ) ;
#18856=CARTESIAN_POINT ( 'NONE',  ( 18.78723038048892846, -5.555560056377619738, 4.275175838841520637 ) ) ;
#18902=ORIENTED_EDGE ( 'NONE', *, *, #28371, .T. ) ;
#18927=CARTESIAN_POINT ( 'NONE',  ( 101.8212854292504090, -4.325038295980876413, -3.539148343398925700 ) ) ;
#18945=CARTESIAN_POINT ( 'NONE',  ( 40.73236281613284149, -5.747100024560975129, 3.993433057584553580 ) ) ;
#18995=CARTESIAN_POINT ( 'NONE',  ( 69.15470699321888048, -7.794592769514103736, -0.8105619180604369811 ) ) ;
#19019=CARTESIAN_POINT ( 'NONE',  ( 28.67557137524189770, -6.315853537245688543, 4.312042181580753031 ) ) ;
#19021=CARTESIAN_POINT ( 'NONE',  ( 69.01977195939538490, -5.101425094635309243, -4.150066331406297770 ) ) ;
#19051=B_SPLINE_CURVE_WITH_KNOTS ( 'NONE', 3,
 ( #25294, #17577, #15076, #11208, #18581, #1194, #28940, #29264, #29117, #3069 ),
 .UNSPECIFIED., .F., .F.,
 ( 4, 3, 3, 4 ),
 ( 0.000000000000000000, 0.0005352024010578534073, 0.001070404802115707682, 0.002130599681840941728 ),
 .UNSPECIFIED. ) ;
#19052=CARTESIAN_POINT ( 'NONE',  ( 69.07040690273157679, -6.115505791281661274, 3.995007138404602198 ) ) ;
#19057=VERTEX_POINT ( 'NONE', #32537 ) ;
#19066=CARTESIAN_POINT ( 'NONE',  ( 68.76824089134483131, -7.257250553459372533, 2.184958019057942735 ) ) ;
#19079=B_SPLINE_SURFACE_WITH_KNOTS ( 'NONE', 3, 3, ( 
 ( #11456, #28835, #13282, #29323, #5931, #11281, #29172, #21651, #16128, #23665 ),
 ( #16445, #6260, #3281, #18490, #3761, #13926, #24148, #31857, #8925, #1275 ),
 ( #13620, #26175, #10791, #19132, #13448, #21006, #26021, #3127, #23824, #26509 ),
 ( #786, #31517, #8297, #28683, #11115, #21311, #5780, #15956, #31366, #8599 ),
 ( #936, #18817, #29020, #3610, #14772, #16800, #4439, #6912, #9425, #24817 ),
 ( #27317, #19640, #22154, #17108, #6603, #4100, #24970, #6759, #17301, #32365 ),
 ( #14616, #32517, #29509, #12257, #29836, #19989, #19304, #1936, #9578, #22468 ) ),
 .UNSPECIFIED., .F., .F., .F.,
 ( 4, 3, 4 ),
 ( 4, 3, 3, 4 ),
 ( -3.163060390574985741E-14, 0.4999999999999841793, 1.000000000000000000 ),
 ( 0.003598893295621919015, 0.5017994466481711102, 0.7508997233244456559, 1.000000000000720313 ),
 .UNSPECIFIED. ) ;
#19092=CARTESIAN_POINT ( 'NONE',  ( 84.96587235352457412, -4.063769032899242184, -4.001039873161198024 ) ) ;
#19109=CARTESIAN_POINT ( 'NONE',  ( 18.75828436641558028, -5.879118399717574661, 3.993434336035622589 ) ) ;
#19123=CARTESIAN_POINT ( 'NONE',  ( 47.99837860531643940, -3.577301031424836353, -2.713652344655540727 ) ) ;
#19132=CARTESIAN_POINT ( 'NONE',  ( 54.89858654026014051, -3.680211708401539106, -0.8105616792978018736 ) ) ;
#19137=CARTESIAN_POINT ( 'NONE',  ( 101.8666520922540002, -4.978306957426977597, 2.487811139442396957 ) ) ;
#19142=CARTESIAN_POINT ( 'NONE',  ( 41.35712849199997976, -8.497574858407940468, -0.07017451552783590674 ) ) ;
#19146=DIRECTION ( 'NONE',  ( -0.9975973382524638833, -0.06927878976713691683, 0.000000000000000000 ) ) ;
#19155=CARTESIAN_POINT ( 'NONE',  ( 18.86054332783516330, -4.736068442360130248, -3.993434336035624366 ) ) ;
#19162=B_SPLINE_CURVE_WITH_KNOTS ( 'NONE', 3,
 ( #22864, #9989, #4996, #7828, #4655, #14828, #32920, #5157 ),
 .UNSPECIFIED., .F., .F.,
 ( 4, 2, 2, 4 ),
 ( 0.000000000000000000, 0.5000000000000000000, 0.7500000000000000000, 1.000000000000000000 ),
 .UNSPECIFIED. ) ;
#19163=VERTEX_POINT ( 'NONE', #28171 ) ;
#19165=CARTESIAN_POINT ( 'NONE',  ( 69.01573535414546257, -5.020529385098173591, 4.074610585184117895 ) ) ;
#19168=CARTESIAN_POINT ( 'NONE',  ( 54.94755432114006766, -5.434540051867444710, -4.093303786133176914 ) ) ;
#19179=CARTESIAN_POINT ( 'NONE',  ( 102.5305753040692878, -0.1042037546421146210, -0.07017451552781628354 ) ) ;
#19204=CARTESIAN_POINT ( 'NONE',  ( 69.07045576165747036, -6.116484151792160873, 3.993434826686585115 ) ) ;
#19239=CARTESIAN_POINT ( 'NONE',  ( 35.34133959475772713, -3.844168172129504679, 0.8105616794551323556 ) ) ;
#19241=CARTESIAN_POINT ( 'NONE',  ( 101.7156419778298471, -2.803798876308493782, 3.841991596727068359 ) ) ;
#19252=CARTESIAN_POINT ( 'NONE',  ( 40.87774300910533753, -5.750695475552364044, -3.996604168388419698 ) ) ;
#19272=CARTESIAN_POINT ( 'NONE',  ( 41.35325844292899689, -7.141637217102140056, 3.390608916434175057 ) ) ;
#19304=CARTESIAN_POINT ( 'NONE',  ( 35.33267181913306842, -4.397467831974085861, -2.184956776455117211 ) ) ;
#19349=CARTESIAN_POINT ( 'NONE',  ( 54.97582481754341899, -6.455996908956627145, -4.074610066671311870 ) ) ;
#19356=CARTESIAN_POINT ( 'NONE',  ( 18.86054332783516330, -4.736068442360130248, -3.993434336035624366 ) ) ;
#19373=ORIENTED_EDGE ( 'NONE', *, *, #6641, .T. ) ;
#19391=CARTESIAN_POINT ( 'NONE',  ( 69.07035661562366613, -6.114499741367263042, 3.996605157046045687 ) ) ;
#19405=EDGE_LOOP ( 'NONE', ( #20250, #2434, #32196, #4150 ) ) ;
#19427=CARTESIAN_POINT ( 'NONE',  ( 54.89716490668162407, -3.628845007888942042, 0.4367666026990714156 ) ) ;
#19443=CARTESIAN_POINT ( 'NONE',  ( 102.3441187013863356, -2.856883908061261579, -3.996604656719260351 ) ) ;
#19460=CARTESIAN_POINT ( 'NONE',  ( 101.8797206818347973, -5.166491396334524033, 2.184956718991889257 ) ) ;
#19470=ORIENTED_EDGE ( 'NONE', *, *, #8358, .F. ) ;
#19496=CARTESIAN_POINT ( 'NONE',  ( 23.61221640758335027, -8.051464822112823327, -0.07017451552783526836 ) ) ;
#19518=CARTESIAN_POINT ( 'NONE',  ( 102.4077201195266440, -3.775001509843904479, -4.215290384275154345 ) ) ;
#19526=EDGE_CURVE ( 'NONE', #15360, #18631, #23434, .T. ) ;
#19542=CARTESIAN_POINT ( 'NONE',  ( 18.93617721851659041, -3.890633339435721982, -4.522129901861162260 ) ) ;
#19544=CARTESIAN_POINT ( 'NONE',  ( 35.27668332986760191, -7.991339570345005860, 1.873789188799038774 ) ) ;
#19549=CARTESIAN_POINT ( 'NONE',  ( 18.75915348114306269, -5.869403441360198315, 4.008637382310625163 ) ) ;
#19567=VERTEX_POINT ( 'NONE', #21600 ) ;
#19578=FACE_OUTER_BOUND ( 'NONE', #5590, .T. ) ;
#19588=ORIENTED_EDGE ( 'NONE', *, *, #30787, .F. ) ;
#19592=CARTESIAN_POINT ( 'NONE',  ( 54.94552861322679149, -5.361349067125541268, -3.996604662717867740 ) ) ;
#19598=CARTESIAN_POINT ( 'NONE',  ( 48.08400536259535585, -8.675012021211061963, -2.713652344655542059 ) ) ;
#19612=EDGE_CURVE ( 'NONE', #29154, #256, #30304, .T. ) ;
#19631=EDGE_LOOP ( 'NONE', ( #21798, #31322, #18535, #8156, #11067, #4268, #30535, #21041, #19373, #23717, #8023, #9713 ) ) ;
#19640=CARTESIAN_POINT ( 'NONE',  ( 84.88357813086332726, -2.741221277473834483, -1.873788409403105426 ) ) ;
#19643=B_SPLINE_CURVE_WITH_KNOTS ( 'NONE', 3,
 ( #13709, #11828, #24871, #31620, #8380, #28767, #5303, #9982 ),
 .UNSPECIFIED., .F., .F.,
 ( 4, 2, 2, 4 ),
 ( 0.009524646911531405372, 0.5047623234557655492, 0.7523811617278827191, 1.000000000000000000 ),
 .UNSPECIFIED. ) ;
#19668=ADVANCED_FACE ( 'NONE', ( #32924 ), #929, .T. ) ;
#19672=CARTESIAN_POINT ( 'NONE',  ( 18.86054332783663767, -4.736068442360260811, 3.993434336035622589 ) ) ;
#19674=CARTESIAN_POINT ( 'NONE',  ( 85.03579748203488009, -5.204477564382398391, -3.993433529979800056 ) ) ;
#19707=CARTESIAN_POINT ( 'NONE',  ( 69.07029661791293051, -6.113298883570701392, 3.998506773566581352 ) ) ;
#19711=LINE ( 'NONE', #20063, #16106 ) ;
#19734=CARTESIAN_POINT ( 'NONE',  ( 68.95644445485396545, -3.844730188642862423, 2.184957270839068322 ) ) ;
#19737=CARTESIAN_POINT ( 'NONE',  ( 101.6895021285839391, -2.427391549943337612, 3.236220879366405789 ) ) ;
#19748=CARTESIAN_POINT ( 'NONE',  ( 28.69351768328725782, -5.618942245713509642, -3.998506281427256948 ) ) ;
#19752=CARTESIAN_POINT ( 'NONE',  ( 41.43141396789280151, -2.886852813799071438, 0.07017451552782173751 ) ) ;
#19795=ADVANCED_FACE ( 'NONE', ( #14784, #20310 ), #27508, .T. ) ;
#19812=DIRECTION ( 'NONE',  ( -0.9960221812693187404, 0.08910563629484180570, 0.000000000000000000 ) ) ;
#19843=CARTESIAN_POINT ( 'NONE',  ( 18.75828436641558028, -5.879118399717574661, -3.993434336035625254 ) ) ;
#19859=ADVANCED_FACE ( 'NONE', ( #12761 ), #28945, .F. ) ;
#19874=CARTESIAN_POINT ( 'NONE',  ( 69.22368686548675498, -4.843077221813552491, -5.695980980372493008 ) ) ;
#19884=CARTESIAN_POINT ( 'NONE',  ( 54.97686130719702646, -6.493447402409093350, 4.013697991739336501 ) ) ;
#19900=ORIENTED_EDGE ( 'NONE', *, *, #19526, .F. ) ;
#19923=CARTESIAN_POINT ( 'NONE',  ( 47.88345462389486329, -3.874360026377489774, 0.8105615593680149944 ) ) ;
#19938=CARTESIAN_POINT ( 'NONE',  ( 54.94642964003813290, -5.393904110543447317, -4.043900691114545864 ) ) ;
#19942=CARTESIAN_POINT ( 'NONE',  ( 29.41391112839824373, -2.700987858903443950, 0.07017451552782173751 ) ) ;
#19989=CARTESIAN_POINT ( 'NONE',  ( 41.34552818481519409, -4.491668296270788119, -2.184957213353903693 ) ) ;
#19992=CARTESIAN_POINT ( 'NONE',  ( 85.49734435724840864, -7.913007294147472059, 0.07017451552781736601 ) ) ;
#20001=CARTESIAN_POINT ( 'NONE',  ( 47.75999538435722513, -8.435302152663906483, 0.02339150517593243869 ) ) ;
#20003=CARTESIAN_POINT ( 'NONE',  ( 68.56906952848913761, -3.255983411058663179, -0.02339150518254430253 ) ) ;
#20011=B_SPLINE_CURVE_WITH_KNOTS ( 'NONE', 3,
 ( #16774, #14092, #24292, #1406, #11581, #21777, #31986, #9054 ),
 .UNSPECIFIED., .F., .F.,
 ( 4, 2, 2, 4 ),
 ( 0.000000000000000000, 0.5000000000000000000, 0.7500000000000000000, 1.000000000000000000 ),
 .UNSPECIFIED. ) ;
#20020=EDGE_CURVE ( 'NONE', #10748, #22902, #16307, .T. ) ;
#20027=CARTESIAN_POINT ( 'NONE',  ( 69.06417839047257701, -5.990839020724394004, -4.155405370686176880 ) ) ;
#20052=CARTESIAN_POINT ( 'NONE',  ( 69.32965659118902124, -6.955028994473984483, -4.522129901861164036 ) ) ;
#20059=CARTESIAN_POINT ( 'NONE',  ( 54.97711309884392961, -6.502545147706987549, 3.999773680152649558 ) ) ;
#20063=CARTESIAN_POINT ( 'NONE',  ( 102.5305753040692878, -0.1042037546421146210, 0.07017451552781736601 ) ) ;
#20074=CARTESIAN_POINT ( 'NONE',  ( 69.09268213438589612, -2.232183665269761086, 0.07017451552782173751 ) ) ;
#20091=CARTESIAN_POINT ( 'NONE',  ( 102.8580990270160385, -4.820463887425401772, 4.522129901861162260 ) ) ;
#20102=CARTESIAN_POINT ( 'NONE',  ( 84.96723802116302693, -4.086039325506168218, -4.033869228762161363 ) ) ;
#20107=CARTESIAN_POINT ( 'NONE',  ( 41.43219399715333395, -3.145521524160642457, 1.915219082070892531 ) ) ;
#20128=CARTESIAN_POINT ( 'NONE',  ( 101.7221769401408409, -2.897900707892763439, -3.993434276071010203 ) ) ;
#20153=CARTESIAN_POINT ( 'NONE',  ( 23.58234648083524121, -8.048792613698569909, -0.02339150517595086839 ) ) ;
#20168=CARTESIAN_POINT ( 'NONE',  ( 101.7974586501929366, -3.981938604909214696, -4.091315454904098203 ) ) ;
#20170=CARTESIAN_POINT ( 'NONE',  ( 41.20585001718148277, -8.497180311781159290, 0.07017451552781736601 ) ) ;
#20181=CARTESIAN_POINT ( 'NONE',  ( 101.8016823592330127, -4.042758964360499974, 3.993434276137187489 ) ) ;
#20204=CARTESIAN_POINT ( 'NONE',  ( 19.01480233883215476, -3.011762293217291830, 0.4426577273443488281 ) ) ;
#20206=CARTESIAN_POINT ( 'NONE',  ( 41.43709133142961321, -4.769546740945156849, -4.522129901861162260 ) ) ;
#20210=CARTESIAN_POINT ( 'NONE',  ( 28.66435036896872290, -6.755537191812748254, 4.008637382357084888 ) ) ;
#20225=CARTESIAN_POINT ( 'NONE',  ( 54.97742507208618434, -6.506533559248983245, -3.993434333358883759 ) ) ;
#20233=CARTESIAN_POINT ( 'NONE',  ( 54.91409664898025511, -4.233361888145934060, 2.184956776138676116 ) ) ;
#20236=CARTESIAN_POINT ( 'NONE',  ( 41.34386496145464207, -3.886814715717140878, 0.07017451552807979498 ) ) ;
#20237=CARTESIAN_POINT ( 'NONE',  ( 102.9361373302715918, -5.944196040818414239, 2.713652344655544724 ) ) ;
#20248=CARTESIAN_POINT ( 'NONE',  ( 102.3469098519873626, -2.897175310220293731, -4.053847705497527265 ) ) ;
#20250=ORIENTED_EDGE ( 'NONE', *, *, #12921, .T. ) ;
#20255=CARTESIAN_POINT ( 'NONE',  ( 23.57316428367446548, -9.051964865574909425, -1.010822989962099960 ) ) ;
#20258=ORIENTED_EDGE ( 'NONE', *, *, #4891, .F. ) ;
#20294=ORIENTED_EDGE ( 'NONE', *, *, #17352, .F. ) ;
#20310=FACE_OUTER_BOUND ( 'NONE', #19631, .T. ) ;
#20313=EDGE_CURVE ( 'NONE', #17452, #4124, #8256, .T. ) ;
#20337=CARTESIAN_POINT ( 'NONE',  ( 48.09670199522223299, -9.430894477034980738, 1.010822989962089746 ) ) ;
#20344=ORIENTED_EDGE ( 'NONE', *, *, #18095, .F. ) ;
#20348=CARTESIAN_POINT ( 'NONE',  ( 23.68064580653238949, -7.171681651382474598, 4.522129901861162260 ) ) ;
#20350=CARTESIAN_POINT ( 'NONE',  ( 29.38825086720286350, -3.456623792451285482, -2.713652344655540727 ) ) ;
#20370=CARTESIAN_POINT ( 'NONE',  ( 102.6609843814833027, -1.982062027707615082, -4.522129901861162260 ) ) ;
#20374=CARTESIAN_POINT ( 'NONE',  ( 69.06873112120143787, -6.081964788647525211, 4.043901188644938749 ) ) ;
#20424=CARTESIAN_POINT ( 'NONE',  ( 69.01370136936026256, -4.979762270910514488, -4.008637876656666599 ) ) ;
#20432=CARTESIAN_POINT ( 'NONE',  ( 85.49734435724778336, -7.913007294147514692, -0.07017451552783579571 ) ) ;
#20443=FACE_OUTER_BOUND ( 'NONE', #6199, .T. ) ;
#20454=ORIENTED_EDGE ( 'NONE', *, *, #27117, .T. ) ;
#20467=CARTESIAN_POINT ( 'NONE',  ( 29.18953645666585217, -9.308308156628569918, -0.07017451552783579571 ) ) ;
#20495=CARTESIAN_POINT ( 'NONE',  ( 68.79832465278998654, -7.861404707920828905, -0.07017451552783579571 ) ) ;
#20498=CARTESIAN_POINT ( 'NONE',  ( 54.64624227588102201, -3.635739347938792054, -0.02339150518254430253 ) ) ;
#20510=CARTESIAN_POINT ( 'NONE',  ( 102.5305753040692878, -0.1042037546421146210, -0.07017451552781628354 ) ) ;
#20512=CARTESIAN_POINT ( 'NONE',  ( 69.09268213438589612, -2.232183665269756645, -1.010822989962086416 ) ) ;
#20520=DIRECTION ( 'NONE',  ( 0.000000000000000000, 0.000000000000000000, 1.000000000000000000 ) ) ;
#20525=CARTESIAN_POINT ( 'NONE',  ( 102.9361373302715918, -5.944196040818414239, 2.713652344655544724 ) ) ;
#20527=ADVANCED_FACE ( 'NONE', ( #735 ), #13715, .F. ) ;
#20555=CARTESIAN_POINT ( 'NONE',  ( 18.76206016059314763, -5.836912598754047998, 4.053847714184954931 ) ) ;
#20579=CARTESIAN_POINT ( 'NONE',  ( 28.70307564580985371, -5.239617037324004301, 3.390608483623311908 ) ) ;
#20583=CARTESIAN_POINT ( 'NONE',  ( 18.61776180080997989, -7.449878658335503445, 1.169950778988562146 ) ) ;
#20588=CARTESIAN_POINT ( 'NONE',  ( 23.90742340929273624, -3.204431202270332513, 2.713652344655542503 ) ) ;
#20594=CARTESIAN_POINT ( 'NONE',  ( 84.97362918700360979, -4.190265677326723726, -4.150065216340092178 ) ) ;
#20638=VERTEX_POINT ( 'NONE', #2794 ) ;
#20659=CARTESIAN_POINT ( 'NONE',  ( 23.84714171513300229, -3.444070612154822353, 0.07017451549163798707 ) ) ;
#20691=CARTESIAN_POINT ( 'NONE',  ( 41.44567272411835290, -7.615257740949710197, 4.522129901861162260 ) ) ;
#20692=CARTESIAN_POINT ( 'NONE',  ( 47.94950013216721629, -7.827917879355752007, -2.184956529945580872 ) ) ;
#20713=CARTESIAN_POINT ( 'NONE',  ( 54.97358454004179151, -6.375051295539742924, 4.150065907150774613 ) ) ;
#20726=CARTESIAN_POINT ( 'NONE',  ( 29.22961111230330999, -6.951722887053946032, -3.390608046110267004 ) ) ;
#20732=ADVANCED_FACE ( 'NONE', ( #31220 ), #19079, .F. ) ;
#20740=ORIENTED_EDGE ( 'NONE', *, *, #31868, .T. ) ;
#20742=DIRECTION ( 'NONE',  ( -0.9975973382524639943, -0.06927878976713693071, 0.000000000000000000 ) ) ;
#20747=CARTESIAN_POINT ( 'NONE',  ( 69.02444692758074041, -5.195103839413598656, -4.215290682810015177 ) ) ;
#20753=CARTESIAN_POINT ( 'NONE',  ( 23.58793147791972444, -8.793627369988310960, -1.915219082070897638 ) ) ;
#20770=CARTESIAN_POINT ( 'NONE',  ( 101.8016823592330127, -4.042758964360499974, 3.993434276137187489 ) ) ;
#20778=CARTESIAN_POINT ( 'NONE',  ( 41.45135008765516460, -9.497951668093163491, -0.07017451552783579571 ) ) ;
#20794=CARTESIAN_POINT ( 'NONE',  ( 18.72498703414868260, -6.251315747377667265, 3.393491514081778071 ) ) ;
#20812=VERTEX_POINT ( 'NONE', #1762 ) ;
#20859=SHAPE_DEFINITION_REPRESENTATION ( #9468, #30799 ) ;
#20862=CARTESIAN_POINT ( 'NONE',  ( 18.76007193770565351, -5.859136940314201070, 4.023790192988138337 ) ) ;
#20869=CARTESIAN_POINT ( 'NONE',  ( 18.76371685223992003, -5.818394111047758166, 4.091315477141354684 ) ) ;
#20878=CARTESIAN_POINT ( 'NONE',  ( 102.4756904796925596, -4.748902435557111446, -2.787782622584134451 ) ) ;
#20898=VERTEX_POINT ( 'NONE', #262 ) ;
#20902=CARTESIAN_POINT ( 'NONE',  ( 28.69165144960210867, -5.691079856418894245, -4.093303788746957217 ) ) ;
#20955=CARTESIAN_POINT ( 'NONE',  ( 18.86054332783663767, -4.736068442360261699, 3.993434336035624366 ) ) ;
#20957=EDGE_CURVE ( 'NONE', #22238, #32480, #2106, .T. ) ;
#20961=AXIS2_PLACEMENT_3D ( 'NONE', #4643, #27383, #4496 ) ;
#20980=CARTESIAN_POINT ( 'NONE',  ( 41.43369393131070666, -3.642920876109168926, 2.713652344655542503 ) ) ;
#21006=CARTESIAN_POINT ( 'NONE',  ( 41.34400607036777586, -3.938209558064118987, -0.8105618912876280113 ) ) ;
#21019=CARTESIAN_POINT ( 'NONE',  ( 85.11758351742656714, -6.522238754303181452, -1.873788413186571189 ) ) ;
#21041=ORIENTED_EDGE ( 'NONE', *, *, #27391, .T. ) ;
#21045=CARTESIAN_POINT ( 'NONE',  ( 18.76498559208903671, -5.804212145908565823, 4.093303788723032355 ) ) ;
#21062=CARTESIAN_POINT ( 'NONE',  ( 54.98781319022972980, -6.881869368919742769, -3.390608480956866178 ) ) ;
#21069=CARTESIAN_POINT ( 'NONE',  ( 69.18703749905368738, -4.112663945019823686, 4.522129901861162260 ) ) ;
#21074=CARTESIAN_POINT ( 'NONE',  ( 85.13967574987862008, -6.881122605237359302, 0.8105612905563517323 ) ) ;
#21081=CARTESIAN_POINT ( 'NONE',  ( 23.84310522038115465, -4.329614468541457484, 4.522129901861162260 ) ) ;
#21087=CARTESIAN_POINT ( 'NONE',  ( 84.97632234719172573, -4.234187385253560088, -4.185347070103271783 ) ) ;
#21129=CARTESIAN_POINT ( 'NONE',  ( 48.06508596181272708, -7.548662730768715079, -4.522129901861164036 ) ) ;
#21131=CARTESIAN_POINT ( 'NONE',  ( 18.88575891862270240, -4.454208744578314949, 3.539106266409321133 ) ) ;
#21141=CARTESIAN_POINT ( 'NONE',  ( 69.08947486655651460, -6.491576118626577241, 3.390608973714449359 ) ) ;
#21157=SHAPE_REPRESENTATION_RELATIONSHIP ( 'NONE' , 'NONE' ,  #30799, #30736 ) ;
#21179=CARTESIAN_POINT ( 'NONE',  ( 55.02116481234001810, -8.082960297851709441, -1.169950777210956083 ) ) ;
#21186=CARTESIAN_POINT ( 'NONE',  ( 102.3434546416268773, -2.854938759700320627, 3.993434327340286583 ) ) ;
#21194=CARTESIAN_POINT ( 'NONE',  ( 54.92448458019108415, -4.608697703005007362, -2.787782628541026320 ) ) ;
#21199=CARTESIAN_POINT ( 'NONE',  ( 102.3664313161174420, -3.178976151102068215, 4.275175836097663051 ) ) ;
#21224=CARTESIAN_POINT ( 'NONE',  ( 102.5330529704723546, -5.572982809272949645, 1.169950773226209106 ) ) ;
#21256=CARTESIAN_POINT ( 'NONE',  ( 101.8016823592329274, -4.042758964359259188, -3.993434276136486716 ) ) ;
#21263=CARTESIAN_POINT ( 'NONE',  ( 101.8016823592330127, -4.042758964360499974, 3.993434276137187489 ) ) ;
#21277=CARTESIAN_POINT ( 'NONE',  ( 18.94426840742758245, -3.800190086666909828, 2.484897251481009040 ) ) ;
#21303=CARTESIAN_POINT ( 'NONE',  ( 29.38825086720286350, -3.456623792451285482, -2.713652344655540727 ) ) ;
#21311=CARTESIAN_POINT ( 'NONE',  ( 41.34428855215451648, -4.040999237037778968, -1.169951068919291348 ) ) ;
#21345=CARTESIAN_POINT ( 'NONE',  ( 28.67878734107726046, -6.190522357109429663, 4.312042181584448741 ) ) ;
#21362=CARTESIAN_POINT ( 'NONE',  ( 55.00858942667153428, -7.632540988256709902, -2.184956776153270219 ) ) ;
#21377=CARTESIAN_POINT ( 'NONE',  ( 18.62691943105422254, -7.347514731317398073, 1.529339877370982981 ) ) ;
#21385=CARTESIAN_POINT ( 'NONE',  ( 54.97720174176811980, -6.505747997631214474, 3.994702633076089082 ) ) ;
#21519=( GEOMETRIC_REPRESENTATION_CONTEXT ( 3 ) GLOBAL_UNCERTAINTY_ASSIGNED_CONTEXT ( ( #27549 ) ) GLOBAL_UNIT_ASSIGNED_CONTEXT ( ( #10458, #28174, #13606 ) ) REPRESENTATION_CONTEXT ( 'NONE', 'WORKASPACE' ) );
#21528=CARTESIAN_POINT ( 'NONE',  ( 84.96867291396014821, -4.109438037582242131, 4.074609222369775630 ) ) ;
#21540=CARTESIAN_POINT ( 'NONE',  ( 18.94410479637168621, -3.802018929891117338, -2.487845153640489748 ) ) ;
#21557=CARTESIAN_POINT ( 'NONE',  ( 41.35542541868176158, -7.892720653454384561, 2.184957211341423733 ) ) ;
#21567=CARTESIAN_POINT ( 'NONE',  ( 85.03570040675890596, -5.202893351561465707, 3.995969900454463986 ) ) ;
#21600=CARTESIAN_POINT ( 'NONE',  ( 18.68265047573912341, -6.724553502642427461, 4.522129901861162260 ) ) ;
#21607=CARTESIAN_POINT ( 'NONE',  ( 28.69349675861934301, -5.619750657913020753, -3.999773682874202319 ) ) ;
#21651=CARTESIAN_POINT ( 'NONE',  ( 29.34042402277824735, -3.698761498129651493, -0.07017451553337591963 ) ) ;
#21655=CARTESIAN_POINT ( 'NONE',  ( 101.9216173105994301, -5.769792427975440674, 0.4426577266272666566 ) ) ;
#21681=CARTESIAN_POINT ( 'NONE',  ( 84.97936832875919322, -4.283865861999379021, 4.215289907553382953 ) ) ;
#21685=CARTESIAN_POINT ( 'NONE',  ( 84.97018126096170931, -4.134036538230700053, -4.093303008782878116 ) ) ;
#21746=B_SPLINE_SURFACE_WITH_KNOTS ( 'NONE', 3, 3, ( 
 ( #27826, #27510, #4943, #7606, #15288, #30026, #12122, #17620, #22318, #15125 ),
 ( #32531, #32873, #25490, #88, #2448, #4454, #25336, #28014, #4609, #30351 ),
 ( #12616, #5110, #20003, #20498, #30712, #2598, #17462, #14786, #24984, #7115 ),
 ( #22817, #9594, #22969, #4765, #14939, #30200, #17316, #10278, #2094, #33022 ) ),
 .UNSPECIFIED., .F., .F., .F.,
 ( 4, 4 ),
 ( 4, 3, 3, 4 ),
 ( 1.412182049029299374E-10, 1.000000000000000000 ),
 ( 0.009544196576262833909, 0.5047720982881089835, 0.7523860491440320653, 0.9999999999999551470 ),
 .UNSPECIFIED. ) ;
#21759=CARTESIAN_POINT ( 'NONE',  ( 40.87773863319960554, -5.749898180376480816, -3.995336175111656285 ) ) ;
#21775=B_SPLINE_CURVE_WITH_KNOTS ( 'NONE', 3,
 ( #887, #13090, #7902, #723, #23432, #13565 ),
 .UNSPECIFIED., .F., .F.,
 ( 4, 2, 4 ),
 ( 0.009527197497156560113, 0.5047635987485782350, 1.000000000000000000 ),
 .UNSPECIFIED. ) ;
#21777=CARTESIAN_POINT ( 'NONE',  ( 29.25343337322282622, -7.426690278353109242, -4.522129901861164036 ) ) ;
#21798=ORIENTED_EDGE ( 'NONE', *, *, #24873, .T. ) ;
#21803=CARTESIAN_POINT ( 'NONE',  ( 101.6441386174529384, -1.774168274679073454, -2.184956718804114573 ) ) ;
#21833=CARTESIAN_POINT ( 'NONE',  ( 69.04806619053955785, -5.668245219738529350, 4.312042181580753031 ) ) ;
#21864=CARTESIAN_POINT ( 'NONE',  ( 29.19739603783667548, -7.896110766392163249, 1.873788768274956995 ) ) ;
#21870=CARTESIAN_POINT ( 'NONE',  ( 102.4231535280176217, -3.997791915949104435, 3.996604656711563397 ) ) ;
#21903=CARTESIAN_POINT ( 'NONE',  ( 84.85832005755366936, -2.331047133796893434, 0.4367664088711343817 ) ) ;
#21910=CARTESIAN_POINT ( 'NONE',  ( 48.01729800609908949, -4.703650321870251894, -4.522129901861162260 ) ) ;
#21920=CARTESIAN_POINT ( 'NONE',  ( 84.96563828038404154, -4.059947112070683595, -3.995005841611614095 ) ) ;
#21953=DIRECTION ( 'NONE',  ( 0.04710975479914575326, 0.5265925107009691297, -0.8488115212910426477 ) ) ;
#21989=VERTEX_POINT ( 'NONE', #15786 ) ;
#22016=CARTESIAN_POINT ( 'NONE',  ( 54.97099024851991800, -6.281314660059669208, -4.215290387854291332 ) ) ;
#22049=EDGE_CURVE ( 'NONE', #29154, #3757, #13253, .T. ) ;
#22051=CARTESIAN_POINT ( 'NONE',  ( 23.64680669414060787, -7.447390197411329460, 2.184956778807267241 ) ) ;
#22058=CARTESIAN_POINT ( 'NONE',  ( 28.66452313916941108, -6.748747283354279425, 4.018750267705075707 ) ) ;
#22096=CARTESIAN_POINT ( 'NONE',  ( 35.33811999951200278, -4.049688432971601415, 1.529339875354069012 ) ) ;
#22110=CARTESIAN_POINT ( 'NONE',  ( 18.86047280610195997, -4.736856733801993791, -3.994702635770043475 ) ) ;
#22124=ORIENTED_EDGE ( 'NONE', *, *, #5217, .F. ) ;
#22134=EDGE_CURVE ( 'NONE', #4533, #256, #10945, .T. ) ;
#22135=CARTESIAN_POINT ( 'NONE',  ( 101.6022419886208610, -1.170867242066746083, -0.4426577266578177183 ) ) ;
#22154=CARTESIAN_POINT ( 'NONE',  ( 68.94677942527458470, -3.651108094208722843, -1.873789666860088632 ) ) ;
#22180=CARTESIAN_POINT ( 'NONE',  ( 101.7221769401408409, -2.897900707892763439, -3.993434276071010203 ) ) ;
#22187=CARTESIAN_POINT ( 'NONE',  ( 28.66410178494867367, -6.765307663812238914, -3.993434336023267139 ) ) ;
#22220=CARTESIAN_POINT ( 'NONE',  ( 85.03457044784497043, -5.184453191149429152, 4.023789378550656437 ) ) ;
#22221=B_SPLINE_CURVE_WITH_KNOTS ( 'NONE', 3,
 ( #13810, #8338, #3654, #24016, #13506, #8181 ),
 .UNSPECIFIED., .F., .F.,
 ( 4, 2, 4 ),
 ( 0.000000000000000000, 0.001111101127398034585, 0.002222202254796068737 ),
 .UNSPECIFIED. ) ;
#22234=DIRECTION ( 'NONE',  ( -0.08910563629484158366, -0.9960221812693186294, 0.000000000000000000 ) ) ;
#22238=VERTEX_POINT ( 'NONE', #10401 ) ;
#22249=CARTESIAN_POINT ( 'NONE',  ( 18.97818541979132334, -3.421065958672417473, 1.873789191073851335 ) ) ;
#22263=CARTESIAN_POINT ( 'NONE',  ( 28.69355920165661900, -5.617338241167577628, -3.995970707775803987 ) ) ;
#22267=CARTESIAN_POINT ( 'NONE',  ( 102.5484925806840977, -0.3622080806379257556, 1.915219082070892531 ) ) ;
#22309=CARTESIAN_POINT ( 'NONE',  ( 18.58227844715246135, -7.846511338401735536, 2.713652344655542503 ) ) ;
#22318=CARTESIAN_POINT ( 'NONE',  ( 23.84714171513466141, -3.444070612163573575, 0.07017451550800275772 ) ) ;
#22339=CARTESIAN_POINT ( 'NONE',  ( 40.88371753250735452, -6.846020710327327841, -4.074609548160287531 ) ) ;
#22352=CARTESIAN_POINT ( 'NONE',  ( 69.13057415542957074, -2.987362752442195291, -2.713652344655540727 ) ) ;
#22370=CARTESIAN_POINT ( 'NONE',  ( 54.97709061282851195, -6.501732682086259096, 4.001040679971932690 ) ) ;
#22400=CARTESIAN_POINT ( 'NONE',  ( 23.86731473547942173, -3.600650094301432791, 1.169950778993111173 ) ) ;
#22418=CARTESIAN_POINT ( 'NONE',  ( 84.96617506415587684, -4.068705388295901670, -4.008636570259113796 ) ) ;
#22468=CARTESIAN_POINT ( 'NONE',  ( 18.96091535641603443, -3.614110606600299924, -2.184956778830001500 ) ) ;
#22471=CARTESIAN_POINT ( 'NONE',  ( 23.84310522038038727, -4.329614468550014195, -4.522129901861162260 ) ) ;
#22484=CARTESIAN_POINT ( 'NONE',  ( 101.9216173105994159, -5.769792427975438898, 0.02339150517593241788 ) ) ;
#22509=CARTESIAN_POINT ( 'NONE',  ( 18.76949126134281087, -5.753847806405374854, -4.155404940063082364 ) ) ;
#22542=CARTESIAN_POINT ( 'NONE',  ( 102.8580990270160385, -4.820463887425400884, -4.522129901861164036 ) ) ;
#22552=CARTESIAN_POINT ( 'NONE',  ( 54.97713542672909171, -6.503351899782645162, 3.998506278707449457 ) ) ;
#22584=CARTESIAN_POINT ( 'NONE',  ( 102.2656009641822692, -1.731193774301682531, 2.184956770134436788 ) ) ;
#22590=CARTESIAN_POINT ( 'NONE',  ( 35.34214449211034292, -3.792788106923193236, 0.4367666027768959958 ) ) ;
#22603=CARTESIAN_POINT ( 'NONE',  ( 40.87784222422364877, -5.768774535592546826, -4.023789691760647713 ) ) ;
#22607=CARTESIAN_POINT ( 'NONE',  ( 85.13613392229180477, -2.069934983084473767, 2.713652344655541615 ) ) ;
#22629=ORIENTED_EDGE ( 'NONE', *, *, #17868, .T. ) ;
#22632=CARTESIAN_POINT ( 'NONE',  ( 101.6022419886208610, -1.170867242066747860, -0.07017451552781628354 ) ) ;
#22642=ORIENTED_EDGE ( 'NONE', *, *, #32853, .T. ) ;
#22725=CARTESIAN_POINT ( 'NONE',  ( 69.07025633558752986, -6.112492629244566267, 3.999774175338361104 ) ) ;
#22747=CARTESIAN_POINT ( 'NONE',  ( 68.95673039201351173, -3.844717801506668753, 2.184957270214452407 ) ) ;
#22751=CARTESIAN_POINT ( 'NONE',  ( 23.61632761762314203, -8.296864917633476111, 2.713652344655544724 ) ) ;
#22760=CARTESIAN_POINT ( 'NONE',  ( 28.69347568615663491, -5.620564795450311735, -4.001040682695108153 ) ) ;
#22763=ADVANCED_FACE ( 'NONE', ( #28082 ), #8917, .F. ) ;
#22800=ORIENTED_EDGE ( 'NONE', *, *, #18352, .F. ) ;
#22817=CARTESIAN_POINT ( 'NONE',  ( 101.6022419886208610, -1.170867242066748304, -0.07017451552781628354 ) ) ;
#22821=ORIENTED_EDGE ( 'NONE', *, *, #31868, .F. ) ;
#22834=CARTESIAN_POINT ( 'NONE',  ( 84.65816297383790356, -6.961284151106942097, 0.07017451552781733826 ) ) ;
#22864=CARTESIAN_POINT ( 'NONE',  ( 102.9361373302715918, -5.944196040818415128, -2.713652344655542947 ) ) ;
#22873=CARTESIAN_POINT ( 'NONE',  ( 102.4214166294606230, -3.972718723526538209, 4.033870034877223176 ) ) ;
#22889=CARTESIAN_POINT ( 'NONE',  ( 29.24242457239609294, -6.576397578955832657, -3.993433898511009605 ) ) ;
#22899=CARTESIAN_POINT ( 'NONE',  ( 84.37491783462779438, -2.359815117480509539, -0.07017451552781631130 ) ) ;
#22900=CARTESIAN_POINT ( 'NONE',  ( 68.92628806523025276, -3.240579989648460835, 0.07017451552782741353 ) ) ;
#22901=CARTESIAN_POINT ( 'NONE',  ( 23.68064580653238949, -7.171681651382474598, 4.522129901861162260 ) ) ;
#22902=VERTEX_POINT ( 'NONE', #9316 ) ;
#22911=CARTESIAN_POINT ( 'NONE',  ( 102.3458556242839563, -2.881957098797790717, -4.033870034884523115 ) ) ;
#22912=ORIENTED_EDGE ( 'NONE', *, *, #12000, .F. ) ;
#22917=CARTESIAN_POINT ( 'NONE',  ( 41.45135008765517881, -9.497951668093163491, -0.07017451552783579571 ) ) ;
#22926=DIRECTION ( 'NONE',  ( 0.06927878976713691683, -0.9975973382524638833, 0.000000000000000000 ) ) ;
#22959=CARTESIAN_POINT ( 'NONE',  ( 18.75828436641558028, -5.879118399717575549, 3.993434336035622589 ) ) ;
#22969=CARTESIAN_POINT ( 'NONE',  ( 68.56906952848913761, -3.255983411058663179, -0.07017451552781628354 ) ) ;
#22986=FACE_OUTER_BOUND ( 'NONE', #19405, .T. ) ;
#22990=ORIENTED_EDGE ( 'NONE', *, *, #922, .T. ) ;
#22996=CARTESIAN_POINT ( 'NONE',  ( 23.61632761762314203, -8.296864917633476111, 2.713652344655544724 ) ) ;
#23035=CARTESIAN_POINT ( 'NONE',  ( 102.4209028682126501, -3.965302267389474888, 4.043900685069918843 ) ) ;
#23068=AXIS2_PLACEMENT_3D ( 'NONE', #10462, #8109, #7623 ) ;
#23087=ORIENTED_EDGE ( 'NONE', *, *, #30385, .F. ) ;
#23089=CARTESIAN_POINT ( 'NONE',  ( 102.3448865208385143, -2.867967694234029530, -4.013697985705315219 ) ) ;
#23119=CARTESIAN_POINT ( 'NONE',  ( 40.73830215457783055, -6.894995700244995085, 3.993433058216659948 ) ) ;
#23146=VERTEX_POINT ( 'NONE', #2631 ) ;
#23163=CARTESIAN_POINT ( 'NONE',  ( 84.65816297383790356, -6.961284151106942097, -0.02339150517595087880 ) ) ;
#23191=CARTESIAN_POINT ( 'NONE',  ( 29.19831543700435716, -9.049787287704361916, 1.915219082070893863 ) ) ;
#23200=CARTESIAN_POINT ( 'NONE',  ( 69.32965659118902124, -6.955028994486257332, 4.522129901861162260 ) ) ;
#23222=CARTESIAN_POINT ( 'NONE',  ( 69.06910216928156387, -6.089391585246120897, 4.033870539709172753 ) ) ;
#23245=CARTESIAN_POINT ( 'NONE',  ( 35.34214449211032871, -3.792788106923192792, 0.07017451552782108526 ) ) ;
#23246=CARTESIAN_POINT ( 'NONE',  ( 29.19213769713835305, -8.050053894909860119, 1.529339505909079966 ) ) ;
#23252=CARTESIAN_POINT ( 'NONE',  ( 102.6421141555943706, -1.710335469228581484, 0.07017451552783579571 ) ) ;
#23257=CARTESIAN_POINT ( 'NONE',  ( 69.01789987928717096, -5.063907424387957157, -4.112224952817434165 ) ) ;
#23260=ADVANCED_FACE ( 'NONE', ( #5298 ), #31902, .F. ) ;
#23295=EDGE_LOOP ( 'NONE', ( #9913, #11943, #859, #30976 ) ) ;
#23308=CARTESIAN_POINT ( 'NONE',  ( 18.65791233782715963, -7.001076235476726417, 2.184956778830005497 ) ) ;
#23314=CARTESIAN_POINT ( 'NONE',  ( 41.35430931302155244, -7.517178856345512195, 2.787783064021091661 ) ) ;
#23322=EDGE_LOOP ( 'NONE', ( #29493, #29405, #15807, #9334 ) ) ;
#23325=ORIENTED_EDGE ( 'NONE', *, *, #30385, .T. ) ;
#23326=CARTESIAN_POINT ( 'NONE',  ( 18.86054332783516330, -4.736068442360130248, -3.993434336035624366 ) ) ;
#23329=CARTESIAN_POINT ( 'NONE',  ( 102.5305753040692736, -0.1042037546421111793, -1.010822989962086416 ) ) ;
#23346=CARTESIAN_POINT ( 'NONE',  ( 55.00869849602045036, -7.632537969515627907, -2.184956776156974811 ) ) ;
#23354=ORIENTED_EDGE ( 'NONE', *, *, #2689, .F. ) ;
#23361=CARTESIAN_POINT ( 'NONE',  ( 68.99418471616998261, -4.594926857587732449, -3.390608975016885296 ) ) ;
#23368=CARTESIAN_POINT ( 'NONE',  ( 40.88303942367309674, -6.721012086063126389, 4.185347298787005066 ) ) ;
#23390=CARTESIAN_POINT ( 'NONE',  ( 35.27024661284173135, -8.402227462205930308, 0.4367666027820644170 ) ) ;
#23397=CARTESIAN_POINT ( 'NONE',  ( 28.60502136296933884, -6.760022240765948709, -3.993434336023340858 ) ) ;
#23402=CARTESIAN_POINT ( 'NONE',  ( 18.85384210216383138, -4.810974696175653875, -4.093303788729898862 ) ) ;
#23408=DIRECTION ( 'NONE',  ( 0.06927878976713820747, -0.9975973382524637723, 0.000000000000000000 ) ) ;
#23432=CARTESIAN_POINT ( 'NONE',  ( 28.57616583554115053, -7.888378049809503523, -2.184956778837684244 ) ) ;
#23434=LINE ( 'NONE', #32995, #2913 ) ;
#23453=DIRECTION ( 'NONE',  ( 0.000000000000000000, 0.000000000000000000, 1.000000000000000000 ) ) ;
#23459=CARTESIAN_POINT ( 'NONE',  ( 18.69136968068891491, -6.627090290235385872, 2.787782631213004514 ) ) ;
#23480=CARTESIAN_POINT ( 'NONE',  ( 69.10564588818930076, -2.490548236270818894, -1.915219082070890755 ) ) ;
#23482=CARTESIAN_POINT ( 'NONE',  ( 68.59913483175071747, -3.860138077750989272, -2.184958020773514420 ) ) ;
#23499=CARTESIAN_POINT ( 'NONE',  ( 18.64064227445962274, -7.194120883406243117, -1.873789191072353644 ) ) ;
#23523=CARTESIAN_POINT ( 'NONE',  ( 54.97647335323577522, -6.479429838881364923, 4.033870040929349976 ) ) ;
#23538=CARTESIAN_POINT ( 'NONE',  ( 85.08237158773125941, -5.954015309899377328, -2.787781826237480054 ) ) ;
#23540=ORIENTED_EDGE ( 'NONE', *, *, #29969, .T. ) ;
#23552=CARTESIAN_POINT ( 'NONE',  ( 29.18862856207581302, -8.152784366139066208, 1.169950487266440575 ) ) ;
#23556=ORIENTED_EDGE ( 'NONE', *, *, #2731, .F. ) ;
#23558=CARTESIAN_POINT ( 'NONE',  ( 69.18703749905368738, -4.112663945013687261, 4.522129901861162260 ) ) ;
#23563=CARTESIAN_POINT ( 'NONE',  ( 54.94664600394312970, -5.401721570094858649, -4.053847711501203932 ) ) ;
#23591=CARTESIAN_POINT ( 'NONE',  ( 101.8343541425947052, -4.513224517051876106, -3.236291054900928721 ) ) ;
#23615=CARTESIAN_POINT ( 'NONE',  ( 101.7221769401408551, -2.897900707893039662, 3.993434276071444078 ) ) ;
#23665=CARTESIAN_POINT ( 'NONE',  ( 19.01480233880980819, -3.011762293215293429, -0.07017451552781921176 ) ) ;
#23667=CARTESIAN_POINT ( 'NONE',  ( 29.18953645666586638, -9.308308156628569918, 0.07017451552781803215 ) ) ;
#23672=CARTESIAN_POINT ( 'NONE',  ( 102.6609843814833027, -1.982062027707616192, 4.522129901861162260 ) ) ;
#23679=CARTESIAN_POINT ( 'NONE',  ( 69.14957877370493122, -7.691922716131041504, -1.169951105765761223 ) ) ;
#23704=CARTESIAN_POINT ( 'NONE',  ( 84.99303864845812484, -4.506833362056713810, 4.312042181588143563 ) ) ;
#23717=ORIENTED_EDGE ( 'NONE', *, *, #392, .T. ) ;
#23720=CARTESIAN_POINT ( 'NONE',  ( 41.35536016469566789, -7.892720495271999148, -2.184957211637544638 ) ) ;
#23727=CARTESIAN_POINT ( 'NONE',  ( 41.43709133142961321, -4.769546740945158625, 4.522129901861162260 ) ) ;
#23735=CARTESIAN_POINT ( 'NONE',  ( 41.35712849199996555, -8.497574858407944021, 0.4367667074078382949 ) ) ;
#23740=CARTESIAN_POINT ( 'NONE',  ( 102.4232086143177582, -3.998587120485036728, 3.995336663074131600 ) ) ;
#23783=DIRECTION ( 'NONE',  ( 0.000000000000000000, 0.000000000000000000, -1.000000000000000000 ) ) ;
#23786=CARTESIAN_POINT ( 'NONE',  ( 69.32965659118902124, -6.955028994473984483, -4.522129901861164036 ) ) ;
#23798=CARTESIAN_POINT ( 'NONE',  ( 29.24242457239596149, -6.576397578954725986, 3.993433898512776636 ) ) ;
#23824=CARTESIAN_POINT ( 'NONE',  ( 23.87320362638740789, -3.497993740947836994, -0.8105616805859642282 ) ) ;
#23833=CARTESIAN_POINT ( 'NONE',  ( 18.61776180081012200, -7.449878658333833670, -1.169950778994415463 ) ) ;
#23843=ORIENTED_EDGE ( 'NONE', *, *, #25526, .F. ) ;
#23851=CARTESIAN_POINT ( 'NONE',  ( 68.95673039202250720, -3.844717801499071719, -2.184957270212465108 ) ) ;
#23856=CARTESIAN_POINT ( 'NONE',  ( 85.01592635901123174, -4.880223576677269470, 4.275175582411163688 ) ) ;
#23862=CARTESIAN_POINT ( 'NONE',  ( 18.78902913792331475, -5.535453558220409853, 4.282233996325129688 ) ) ;
#23883=CARTESIAN_POINT ( 'NONE',  ( 102.5153059484010640, -5.316817625849363793, 1.873789182723388791 ) ) ;
#23889=CARTESIAN_POINT ( 'NONE',  ( 18.75846136547140830, -5.877139905506971296, 3.996604665398700629 ) ) ;
#23936=CARTESIAN_POINT ( 'NONE',  ( 18.91097450938967484, -4.172349046794661120, 3.084778196783016568 ) ) ;
#23945=CARTESIAN_POINT ( 'NONE',  ( 85.03618457008606413, -5.204454441937159892, 3.993433531046222118 ) ) ;
#23953=DIRECTION ( 'NONE',  ( -0.04710975479914572550, -0.5265925107009689077, 0.8488115212910427587 ) ) ;
#23976=CARTESIAN_POINT ( 'NONE',  ( 101.6022419886208610, -1.170867242066747860, -0.07017451552781628354 ) ) ;
#24001=CARTESIAN_POINT ( 'NONE',  ( 40.87842237877963925, -5.874508746777070023, 4.155404504730444870 ) ) ;
#24007=CARTESIAN_POINT ( 'NONE',  ( 18.75828436641558028, -5.879118399717575549, 3.993434336035622589 ) ) ;
#24016=CARTESIAN_POINT ( 'NONE',  ( 18.62684137740528811, -7.348387214320800886, 1.526432259289672855 ) ) ;
#24032=CARTESIAN_POINT ( 'NONE',  ( 23.62691144361181372, -7.794821506209283157, 1.529339877365281763 ) ) ;
#24040=CARTESIAN_POINT ( 'NONE',  ( 54.97719073509556864, -6.505350304057381017, 3.995336669067921953 ) ) ;
#24064=EDGE_CURVE ( 'NONE', #3757, #2205, #19643, .T. ) ;
#24090=CARTESIAN_POINT ( 'NONE',  ( 69.01337413186240610, -4.973203518777342680, -3.998506773567884753 ) ) ;
#24099=CARTESIAN_POINT ( 'NONE',  ( 18.89416411554475062, -4.360255511983738508, 3.387663576533886278 ) ) ;
#24120=CIRCLE ( 'NONE', #28414, 4.999999999999999112 ) ;
#24136=B_SPLINE_SURFACE_WITH_KNOTS ( 'NONE', 1, 3, ( 
 ( #24359, #1978, #4490, #4301, #14479, #32061, #24691, #3995 ),
 ( #19179, #1631, #4142, #1325, #12001, #17348, #1475, #11820 ) ),
 .UNSPECIFIED., .F., .F., .F.,
 ( 2, 2 ),
 ( 4, 2, 2, 4 ),
 ( 0.000000000000000000, 1.000000000000000000 ),
 ( 0.000000000000000000, 0.5000000000000000000, 0.7500000000000000000, 1.000000000000000000 ),
 .UNSPECIFIED. ) ;
#24144=CIRCLE ( 'NONE', #15075, 1.676012832569465205 ) ;
#24148=CARTESIAN_POINT ( 'NONE',  ( 35.34214449212152687, -3.792788106923345559, -0.4367666027766938242 ) ) ;
#24155=CARTESIAN_POINT ( 'NONE',  ( 101.9216173105994443, -5.769792427975438009, 0.07017451552781736601 ) ) ;
#24160=CARTESIAN_POINT ( 'NONE',  ( 47.95950916398559372, -8.432626694227655761, -0.4367665434710258365 ) ) ;
#24175=CARTESIAN_POINT ( 'NONE',  ( 84.48140976240843258, -4.087790770806424057, -3.993432235010177855 ) ) ;
#24178=ORIENTED_EDGE ( 'NONE', *, *, #30056, .F. ) ;
#24184=CARTESIAN_POINT ( 'NONE',  ( 69.04182551544533908, -5.543251471631118754, 4.312042181584448741 ) ) ;
#24189=CARTESIAN_POINT ( 'NONE',  ( 18.83159731376704826, -5.059626785708270624, -4.275175838844416099 ) ) ;
#24222=CARTESIAN_POINT ( 'NONE',  ( 85.11758351742646767, -6.522238754302136954, 1.873788413188252067 ) ) ;
#24260=CARTESIAN_POINT ( 'NONE',  ( 48.09670199522224721, -9.430894477034977186, -0.07017451552783579571 ) ) ;
#24273=CARTESIAN_POINT ( 'NONE',  ( 18.86045606321215118, -4.737043885707785229, -3.995006647709321790 ) ) ;
#24285=VERTEX_POINT ( 'NONE', #8312 ) ;
#24290=DESIGN_CONTEXT ( 'detailed design', #17589, 'design' ) ;
#24292=CARTESIAN_POINT ( 'NONE',  ( 69.32965659118902124, -6.955028994473984483, -4.522129901861164036 ) ) ;
#24348=CARTESIAN_POINT ( 'NONE',  ( 54.94547365669386352, -5.359363431748539242, 3.993434333351774779 ) ) ;
#24350=CARTESIAN_POINT ( 'NONE',  ( 84.97133056964233333, -4.152779584596041573, -4.112223744635283396 ) ) ;
#24359=CARTESIAN_POINT ( 'NONE',  ( 102.5305753040692878, -0.1042037546421146210, 0.07017451552781951707 ) ) ;
#24373=CARTESIAN_POINT ( 'NONE',  ( 18.74780019990318536, -5.996310340153152119, -5.695980980372493008 ) ) ;
#24380=CARTESIAN_POINT ( 'NONE',  ( 102.4232231159381286, -3.998796565576680617, 3.995006639018732653 ) ) ;
#24384=ORIENTED_EDGE ( 'NONE', *, *, #4891, .T. ) ;
#24408=CARTESIAN_POINT ( 'NONE',  ( 102.2233072702346419, -1.127920370132899475, 0.4367666012506544182 ) ) ;
#24414=CARTESIAN_POINT ( 'NONE',  ( 102.5829460782277351, -0.8583298743146002829, -2.713652344655542503 ) ) ;
#24421=CARTESIAN_POINT ( 'NONE',  ( 102.3442575486588737, -2.858888224824346125, -3.999773674151783087 ) ) ;
#24465=ADVANCED_FACE ( 'NONE', ( #6773 ), #8940, .F. ) ;
#24467=DIRECTION ( 'NONE',  ( -0.9975973382524639943, -0.06927878976713693071, 0.000000000000000000 ) ) ;
#24469=CARTESIAN_POINT ( 'NONE',  ( 85.14283307489681363, -6.932413485865820846, -0.07017451552783708635 ) ) ;
#24496=CARTESIAN_POINT ( 'NONE',  ( 18.76278968803789127, -5.828757946052309791, -4.074610069491733988 ) ) ;
#24529=ADVANCED_FACE ( 'NONE', ( #14631 ), #21746, .F. ) ;
#24533=CARTESIAN_POINT ( 'NONE',  ( 85.03550338738804726, -5.199678113354736730, 4.001039873195242791 ) ) ;
#24552=CARTESIAN_POINT ( 'NONE',  ( 102.9361373302715918, -5.944196040818414239, 2.713652344655544724 ) ) ;
#24566=CARTESIAN_POINT ( 'NONE',  ( 29.31981545343394657, -4.303267367674513899, 2.184956339553084437 ) ) ;
#24573=CARTESIAN_POINT ( 'NONE',  ( 69.13057415542958495, -2.987362752436060642, -2.713652344655542503 ) ) ;
#24579=CARTESIAN_POINT ( 'NONE',  ( 102.3440636142975535, -2.856088703579951815, -3.995336663081834772 ) ) ;
#24587=CARTESIAN_POINT ( 'NONE',  ( 69.10564588828751198, -2.490548236270822446, 1.915219082070892531 ) ) ;
#24597=AXIS2_PLACEMENT_3D ( 'NONE', #23252, #20742, #3363 ) ;
#24650=EDGE_CURVE ( 'NONE', #31589, #17452, #32740, .T. ) ;
#24678=CARTESIAN_POINT ( 'NONE',  ( 40.88399151333042170, -6.896594116923616014, -3.993433839952781117 ) ) ;
#24691=CARTESIAN_POINT ( 'NONE',  ( 23.95058674323790271, -2.449331254364353949, 0.07017451552781951707 ) ) ;
#24720=CARTESIAN_POINT ( 'NONE',  ( 102.4226167450245697, -3.990043124566273303, 4.008637373575834495 ) ) ;
#24742=ORIENTED_EDGE ( 'NONE', *, *, #13191, .F. ) ;
#24758=CARTESIAN_POINT ( 'NONE',  ( 18.96091535642496240, -3.614110606601101949, 2.184956778829998836 ) ) ;
#24761=CARTESIAN_POINT ( 'NONE',  ( 41.45135008765517881, -9.497951668093163491, -0.07017451552783579571 ) ) ;
#24773=CARTESIAN_POINT ( 'NONE',  ( 18.86036632877896935, -4.738046936575775803, -3.996604665406715107 ) ) ;
#24800=VERTEX_POINT ( 'NONE', #29482 ) ;
#24817=CARTESIAN_POINT ( 'NONE',  ( 18.99190826319341596, -3.267672110760019510, -1.529339877370962553 ) ) ;
#24834=EDGE_LOOP ( 'NONE', ( #19588, #19900, #16793, #31017, #27467, #727, #27706, #20294, #24178, #22124, #22821, #12023 ) ) ;
#24850=CARTESIAN_POINT ( 'NONE',  ( 54.97722363750290953, -6.506539134337329777, -3.993434333351804977 ) ) ;
#24871=CARTESIAN_POINT ( 'NONE',  ( 68.79832465279001497, -7.861404707920833346, 0.07017451552781736601 ) ) ;
#24873=EDGE_CURVE ( 'NONE', #19567, #7768, #24144, .T. ) ;
#24880=CARTESIAN_POINT ( 'NONE',  ( 102.8074457324386515, -4.091069046465105608, -5.695980980372493008 ) ) ;
#24887=CARTESIAN_POINT ( 'NONE',  ( 18.75864038940818901, -5.875138777191356354, 3.999773682846184730 ) ) ;
#24927=CARTESIAN_POINT ( 'NONE',  ( 84.96597185339788894, -4.065391592161865297, -4.003573871808557172 ) ) ;
#24932=CARTESIAN_POINT ( 'NONE',  ( 102.5305753040692736, -0.1042037546421131222, 1.010822989962091301 ) ) ;
#24939=LINE ( 'NONE', #2554, #8539 ) ;
#24951=CARTESIAN_POINT ( 'NONE',  ( 101.6441386174529384, -1.774168274679073454, -2.184956718804114573 ) ) ;
#24970=CARTESIAN_POINT ( 'NONE',  ( 35.33570769239872789, -4.203675997508360851, -1.873789188777423176 ) ) ;
#24982=CARTESIAN_POINT ( 'NONE',  ( 35.16139127360178662, -8.400504373793673096, -0.02339150517595086839 ) ) ;
#24984=CARTESIAN_POINT ( 'NONE',  ( 23.84714171513466141, -3.444070612163574463, -0.02339150518254430253 ) ) ;
#24995=CARTESIAN_POINT ( 'NONE',  ( 101.7539452112899170, -3.355355909486178234, -4.312047644358228737 ) ) ;
#25013=B_SPLINE_CURVE_WITH_KNOTS ( 'NONE', 3,
 ( #21256, #11392, #18737, #18927, #13224, #23591, #26109, #16241, #3553, #3698 ),
 .UNSPECIFIED., .F., .F.,
 ( 4, 3, 3, 4 ),
 ( 0.000000000000000000, 0.0005352024010578549252, 0.001070404802115705514, 0.002130599829431759334 ),
 .UNSPECIFIED. ) ;
#25026=CARTESIAN_POINT ( 'NONE',  ( 41.44346753120585447, -6.883984642623638628, -5.695980980372493008 ) ) ;
#25030=CARTESIAN_POINT ( 'NONE',  ( 19.01015279934141589, -3.063734813013466951, 0.8134928201657850577 ) ) ;
#25034=CARTESIAN_POINT ( 'NONE',  ( 69.06980207411518791, -6.103400497572641470, 4.013698489646581713 ) ) ;
#25061=CARTESIAN_POINT ( 'NONE',  ( 69.01291188534348464, -4.970031385439517280, 3.993434827421580735 ) ) ;
#25065=CARTESIAN_POINT ( 'NONE',  ( 84.86779539659983129, -2.484919561749620698, 1.169950239652608914 ) ) ;
#25081=CARTESIAN_POINT ( 'NONE',  ( 102.3453678278643508, -2.874915557871456251, -4.023790184234727896 ) ) ;
#25087=CARTESIAN_POINT ( 'NONE',  ( 19.08086296608604826, -2.273337061837033879, 1.915219082070892531 ) ) ;
#25148=DIRECTION ( 'NONE',  ( -0.08910563629484180570, -0.9960221812693186294, 0.000000000000000000 ) ) ;
#25176=CARTESIAN_POINT ( 'NONE',  ( 54.97374409962333175, -6.380816387357196362, -4.155404937707912971 ) ) ;
#25189=CARTESIAN_POINT ( 'NONE',  ( 101.6702787251852698, -2.150579323183733571, -2.790733426243898752 ) ) ;
#25196=B_SPLINE_CURVE_WITH_KNOTS ( 'NONE', 3,
 ( #20770, #18252, #25961, #23119, #3070, #238 ),
 .UNSPECIFIED., .F., .F.,
 ( 4, 2, 4 ),
 ( 0.009531916414649947711, 0.5047659582073249496, 1.000000000000000000 ),
 .UNSPECIFIED. ) ;
#25219=CARTESIAN_POINT ( 'NONE',  ( 54.97715759724685824, -6.504152965876262016, 3.997238534709005364 ) ) ;
#25244=AXIS2_PLACEMENT_3D ( 'NONE', #30945, #209, #10691 ) ;
#25248=CARTESIAN_POINT ( 'NONE',  ( 28.71260074196063528, -4.863490077431325886, 2.787782631230470543 ) ) ;
#25268=CARTESIAN_POINT ( 'NONE',  ( 54.94560668507518386, -5.364169883902320635, -4.001040679979973369 ) ) ;
#25274=CARTESIAN_POINT ( 'NONE',  ( 69.13057415542958495, -2.987362752442198843, 2.713652344655541615 ) ) ;
#25284=CARTESIAN_POINT ( 'NONE',  ( 18.65791233782715963, -7.001076235476726417, -2.184956778830003277 ) ) ;
#25294=CARTESIAN_POINT ( 'NONE',  ( 18.75828436641558028, -5.879118399717574661, -3.993434336035625254 ) ) ;
#25312=ORIENTED_EDGE ( 'NONE', *, *, #20020, .T. ) ;
#25336=CARTESIAN_POINT ( 'NONE',  ( 35.23476908784418526, -3.791088091780328906, 0.02339150516272998567 ) ) ;
#25339=CARTESIAN_POINT ( 'NONE',  ( 69.32965659118902124, -6.955028994473984483, 4.522129901861163148 ) ) ;
#25354=CARTESIAN_POINT ( 'NONE',  ( 23.58234648083524121, -8.048792613698569909, 0.07017451552781736601 ) ) ;
#25370=CARTESIAN_POINT ( 'NONE',  ( 18.68265047573912341, -6.724553502642427461, 4.522129901861162260 ) ) ;
#25387=CARTESIAN_POINT ( 'NONE',  ( 18.96091535642496240, -3.614110606601101949, 2.184956778829998836 ) ) ;
#25388=CARTESIAN_POINT ( 'NONE',  ( 69.18703749905368738, -4.112663945013685485, -4.522129901861162260 ) ) ;
#25392=CARTESIAN_POINT ( 'NONE',  ( 28.66601932953619425, -6.689973454712867529, 4.093303788750745298 ) ) ;
#25401=CARTESIAN_POINT ( 'NONE',  ( 102.8580990270160385, -4.820463887425400884, -4.522129901861164036 ) ) ;
#25417=CARTESIAN_POINT ( 'NONE',  ( 40.87760899950266946, -5.748707280015221244, 3.993433839266994578 ) ) ;
#25419=CARTESIAN_POINT ( 'NONE',  ( 41.19430503358938012, -3.886431767412240390, -0.07017451552781626967 ) ) ;
#25421=CARTESIAN_POINT ( 'NONE',  ( 48.06508596181272708, -7.548662730762578654, 4.522129901861162260 ) ) ;
#25424=B_SPLINE_CURVE_WITH_KNOTS ( 'NONE', 3,
 ( #30892, #12646, #23200, #15317, #20691, #17494, #20348, #25370 ),
 .UNSPECIFIED., .F., .F.,
 ( 4, 2, 2, 4 ),
 ( 0.000000000000000000, 0.5000000000000000000, 0.7500000000000000000, 1.000000000000000000 ),
 .UNSPECIFIED. ) ;
#25431=CARTESIAN_POINT ( 'NONE',  ( 84.96680598075437274, -4.078993907564744781, -4.023789378516497983 ) ) ;
#25480=CARTESIAN_POINT ( 'NONE',  ( 69.42401195566040428, -8.835509274236315491, 0.07017451552781736601 ) ) ;
#25490=CARTESIAN_POINT ( 'NONE',  ( 68.56906952848913761, -3.255983411058662291, 0.02339150516273700783 ) ) ;
#25514=CARTESIAN_POINT ( 'NONE',  ( 41.44907012423725234, -8.741883605793594469, 2.713652344655544724 ) ) ;
#25519=CARTESIAN_POINT ( 'NONE',  ( 101.7699140880832402, -3.585303762756002932, 4.312047644407677183 ) ) ;
#25526=EDGE_CURVE ( 'NONE', #11659, #4124, #28692, .T. ) ;
#25544=CARTESIAN_POINT ( 'NONE',  ( 54.97561860524439936, -6.448546075709844949, 4.073741752267325822 ) ) ;
#25546=CARTESIAN_POINT ( 'NONE',  ( 18.96091535642496240, -3.614110606601104614, -2.184956778830005053 ) ) ;
#25570=CARTESIAN_POINT ( 'NONE',  ( 102.3175034158304015, -2.480357097896682905, 3.390608474933819672 ) ) ;
#25578=CARTESIAN_POINT ( 'NONE',  ( 69.13057415542958495, -2.987362752442197955, 2.713652344655542503 ) ) ;
#25585=CARTESIAN_POINT ( 'NONE',  ( 102.3446554920049465, -2.864632698915883235, -4.008637373583407992 ) ) ;
#25620=CARTESIAN_POINT ( 'NONE',  ( 23.57316428367674277, -9.051964865549241068, 0.07017451552781736601 ) ) ;
#25625=VERTEX_POINT ( 'NONE', #12851 ) ;
#25626=CARTESIAN_POINT ( 'NONE',  ( 29.21519671786122885, -8.552672223064927692, 2.713652344655544724 ) ) ;
#25652=CARTESIAN_POINT ( 'NONE',  ( 18.87102749435254267, -4.618876501925000433, 5.695980980372492120 ) ) ;
#25666=CARTESIAN_POINT ( 'NONE',  ( 41.43141396789280151, -2.886852813799071438, -0.07017451552781585333 ) ) ;
#25667=CARTESIAN_POINT ( 'NONE',  ( 47.75999538435722513, -8.435302152663906483, 0.07017451552781736601 ) ) ;
#25670=CARTESIAN_POINT ( 'NONE',  ( 102.5829460782277351, -0.8583298743146007270, 2.713652344655542503 ) ) ;
#25672=CARTESIAN_POINT ( 'NONE',  ( 18.60402535543785518, -7.603424548862136589, -0.07017451552783579571 ) ) ;
#25688=CARTESIAN_POINT ( 'NONE',  ( 23.64680669417294823, -7.447390197414223145, -2.184956778807263689 ) ) ;
#25712=LINE ( 'NONE', #15688, #9154 ) ;
#25715=CARTESIAN_POINT ( 'NONE',  ( 54.97605132184205701, -6.464180995122740470, 4.053847711493757444 ) ) ;
#25749=CARTESIAN_POINT ( 'NONE',  ( 47.95525692263736062, -8.175714017049896754, 1.529339665918354241 ) ) ;
#25764=CARTESIAN_POINT ( 'NONE',  ( 84.98546029192083040, -4.383222815415539486, -4.275175582409524999 ) ) ;
#25774=PRODUCT_DEFINITION ( 'UNKNOWN', '', #1293, #24290 ) ;
#25815=VERTEX_POINT ( 'NONE', #1835 ) ;
#25834=CARTESIAN_POINT ( 'NONE',  ( 102.4756904796924033, -4.748902435568509439, 2.787782622565551538 ) ) ;
#25844=CARTESIAN_POINT ( 'NONE',  ( 29.27825211595694554, -6.695835137279974703, 5.695980980372492120 ) ) ;
#25866=CARTESIAN_POINT ( 'NONE',  ( 48.08400536259535585, -8.675012021211058411, 2.713652344655544724 ) ) ;
#25899=CARTESIAN_POINT ( 'NONE',  ( 18.76665878146132371, -5.785509246780520698, 4.112224495634847266 ) ) ;
#25926=CARTESIAN_POINT ( 'NONE',  ( 102.5401559989745408, -5.675509796545467722, 0.8105616764185750167 ) ) ;
#25937=CARTESIAN_POINT ( 'NONE',  ( 18.85676753365875413, -4.778274243329593496, -4.053847714192347240 ) ) ;
#25961=CARTESIAN_POINT ( 'NONE',  ( 68.71221462756291487, -6.131929330199175077, 3.993435576830336231 ) ) ;
#25976=CARTESIAN_POINT ( 'NONE',  ( 102.9361373302715918, -5.944196040818414239, 2.713652344655544724 ) ) ;
#25980=CARTESIAN_POINT ( 'NONE',  ( 85.38119660045754244, -6.034158634414237277, -4.522129901861164036 ) ) ;
#25983=CARTESIAN_POINT ( 'NONE',  ( 18.92762145840779553, -3.986269566730710867, 2.784837724132013026 ) ) ;
#25985=ORIENTED_EDGE ( 'NONE', *, *, #9549, .T. ) ;
#26010=CARTESIAN_POINT ( 'NONE',  ( 18.85511084201081289, -4.796792731029945855, -4.091315477141356460 ) ) ;
#26012=CARTESIAN_POINT ( 'NONE',  ( 85.10544820223228157, -1.573551533641234901, -1.915219082070890755 ) ) ;
#26021=CARTESIAN_POINT ( 'NONE',  ( 35.34133959476921660, -3.844168172129591277, -0.8105616794546218751 ) ) ;
#26032=CARTESIAN_POINT ( 'NONE',  ( 29.19739603781543025, -7.896110766395437963, -1.873788768280044925 ) ) ;
#26047=CARTESIAN_POINT ( 'NONE',  ( 84.94207106226485848, -3.684213880882921899, -3.390607676403233128 ) ) ;
#26051=CARTESIAN_POINT ( 'NONE',  ( 85.03413872134471774, -5.177407751507606903, 4.033869228796232775 ) ) ;
#26073=CARTESIAN_POINT ( 'NONE',  ( 47.68482864957484679, -3.825617316378891797, -0.07017451552781625579 ) ) ;
#26081=CARTESIAN_POINT ( 'NONE',  ( 101.9216173105994585, -5.769792427975423799, -0.4426577264581311733 ) ) ;
#26086=CARTESIAN_POINT ( 'NONE',  ( 54.95033023691122764, -5.534837039125057423, -4.185347662766374377 ) ) ;
#26109=CARTESIAN_POINT ( 'NONE',  ( 101.8408884992664980, -4.607317627582337316, -3.084862410648784969 ) ) ;
#26131=CARTESIAN_POINT ( 'NONE',  ( 102.9361373302715918, -5.944196040818415128, -2.713652344655543391 ) ) ;
#26140=CARTESIAN_POINT ( 'NONE',  ( 101.6022419886208468, -1.170867242066747638, 0.4426577264886745189 ) ) ;
#26145=CARTESIAN_POINT ( 'NONE',  ( 29.21679767122600069, -7.327048195461536295, 2.787782193693228994 ) ) ;
#26152=CARTESIAN_POINT ( 'NONE',  ( 29.38825086720287771, -3.456623792456554156, 2.713652344655542503 ) ) ;
#26175=CARTESIAN_POINT ( 'NONE',  ( 84.86147853072903047, -2.382337935102287307, -0.8105612886928852401 ) ) ;
#26186=CARTESIAN_POINT ( 'NONE',  ( 102.5330529704722125, -5.572982809271280757, -1.169950773232049102 ) ) ;
#26208=CIRCLE ( 'NONE', #32632, 4.999999999999999112 ) ;
#26210=CARTESIAN_POINT ( 'NONE',  ( 84.97327636560633835, -4.184508908553603135, 4.155404232685564914 ) ) ;
#26225=CARTESIAN_POINT ( 'NONE',  ( 85.10546509785196179, -6.328795743799873641, -2.184955973843232258 ) ) ;
#26243=CARTESIAN_POINT ( 'NONE',  ( 102.5437075123492008, -5.726773290143887252, 0.4367666012699079059 ) ) ;
#26305=CARTESIAN_POINT ( 'NONE',  ( 48.08400536259535585, -8.675012021204926427, -2.713652344655543391 ) ) ;
#26324=CARTESIAN_POINT ( 'NONE',  ( 85.08237158772919884, -5.954015309888582408, 2.787781826238851401 ) ) ;
#26329=EDGE_LOOP ( 'NONE', ( #31838, #11801, #32633, #18553 ) ) ;
#26360=CARTESIAN_POINT ( 'NONE',  ( 19.10390797508231131, -2.015740111943978619, -0.07017451552781628354 ) ) ;
#26367=CARTESIAN_POINT ( 'NONE',  ( 35.27971914370662887, -7.797547734959323407, -2.184956776477516183 ) ) ;
#26397=CARTESIAN_POINT ( 'NONE',  ( 102.3749895180304605, -3.302517831815073190, 4.312042181588143563 ) ) ;
#26424=FACE_OUTER_BOUND ( 'NONE', #1572, .T. ) ;
#26459=ORIENTED_EDGE ( 'NONE', *, *, #24064, .T. ) ;
#26492=ORIENTED_EDGE ( 'NONE', *, *, #9549, .F. ) ;
#26509=CARTESIAN_POINT ( 'NONE',  ( 19.01022352368569557, -3.062944256724156489, -0.8105616806061153312 ) ) ;
#26519=CARTESIAN_POINT ( 'NONE',  ( 29.18336473368350070, -8.306880066003914820, -0.07017451552783354751 ) ) ;
#26539=CARTESIAN_POINT ( 'NONE',  ( 54.96134875812031595, -5.932951279990229310, 4.312042181584448741 ) ) ;
#26548=CARTESIAN_POINT ( 'NONE',  ( 18.95251007638874441, -3.708064768245253884, -2.336400966235247623 ) ) ;
#26568=ORIENTED_EDGE ( 'NONE', *, *, #17352, .T. ) ;
#26573=CARTESIAN_POINT ( 'NONE',  ( 54.97722363747754315, -6.506539134378061640, 3.993434333287562144 ) ) ;
#26587=CARTESIAN_POINT ( 'NONE',  ( 84.62099044691464655, -6.357652361207289715, 2.184954680079133293 ) ) ;
#26612=CARTESIAN_POINT ( 'NONE',  ( 84.96567518654291007, -4.060553804896915864, -3.995969900420532461 ) ) ;
#26626=CARTESIAN_POINT ( 'NONE',  ( 41.35220755422911054, -6.766095577562686536, 3.993434768846746419 ) ) ;
#26643=CARTESIAN_POINT ( 'NONE',  ( 19.08086296608603405, -2.273337061837030326, -1.915219082070890755 ) ) ;
#26660=CARTESIAN_POINT ( 'NONE',  ( 18.60402535544292490, -7.603424548862588672, -0.4367666033500683942 ) ) ;
#26683=CARTESIAN_POINT ( 'NONE',  ( 102.3836362560106465, -3.427337902231936351, 4.312042181584448741 ) ) ;
#26685=CARTESIAN_POINT ( 'NONE',  ( 28.69250200978156329, -5.658193782479810530, -4.053847714210987441 ) ) ;
#26709=CARTESIAN_POINT ( 'NONE',  ( 23.84310522038115465, -4.329614468541457484, 4.522129901861162260 ) ) ;
#26725=CARTESIAN_POINT ( 'NONE',  ( 69.07037654389817760, -6.114898606693179417, 3.995971199216228786 ) ) ;
#26774=CARTESIAN_POINT ( 'NONE',  ( 40.87774520873607287, -5.751096254936027385, -3.997238040213327626 ) ) ;
#26775=ORIENTED_EDGE ( 'NONE', *, *, #32172, .T. ) ;
#26789=ORIENTED_EDGE ( 'NONE', *, *, #11160, .T. ) ;
#26841=DIRECTION ( 'NONE',  ( 0.03662738895564522645, -0.5274252892134372317, -0.8488115212910425367 ) ) ;
#26842=CARTESIAN_POINT ( 'NONE',  ( 102.7595417042496706, -3.401262957566509204, 3.636029349014984202 ) ) ;
#26852=CARTESIAN_POINT ( 'NONE',  ( 40.73236281613230148, -5.747100024567912691, -3.993433057586367241 ) ) ;
#26862=CARTESIAN_POINT ( 'NONE',  ( 84.96557803822085475, -4.058969597120936079, 3.993433529938030357 ) ) ;
#26865=CARTESIAN_POINT ( 'NONE',  ( 28.69116527693491392, -5.709888947837792550, -4.112224495657437195 ) ) ;
#26878=B_SPLINE_CURVE_WITH_KNOTS ( 'NONE', 3,
 ( #24155, #21655, #31862, #14122, #3949, #27001 ),
 .UNSPECIFIED., .F., .F.,
 ( 4, 2, 4 ),
 ( 0.000000000000000000, 0.001111101121321064278, 0.002222202242642128556 ),
 .UNSPECIFIED. ) ;
#26899=CARTESIAN_POINT ( 'NONE',  ( 41.44567272411835290, -7.615257740949710197, -4.522129901861164036 ) ) ;
#26909=CARTESIAN_POINT ( 'NONE',  ( 28.66413209314083588, -6.764116340039933561, 3.995336671804473383 ) ) ;
#26939=CARTESIAN_POINT ( 'NONE',  ( 29.32642088966447602, -4.109531239332479657, 1.873788766282109552 ) ) ;
#26953=CARTESIAN_POINT ( 'NONE',  ( 69.01326405434069500, -4.970996605387691503, -3.995007138417703718 ) ) ;
#26954=ORIENTED_EDGE ( 'NONE', *, *, #29522, .F. ) ;
#26987=CARTESIAN_POINT ( 'NONE',  ( 102.5829460782277209, -0.8583298743145987286, -2.713652344655540727 ) ) ;
#27001=CARTESIAN_POINT ( 'NONE',  ( 101.8797206818347973, -5.166491396334524033, 2.184956718991889257 ) ) ;
#27005=CARTESIAN_POINT ( 'NONE',  ( 35.27024661284173845, -8.402227462205928532, -0.4367666027840573229 ) ) ;
#27008=CARTESIAN_POINT ( 'NONE',  ( 18.65837979360809840, -6.995851018290569989, -0.07017451552783644797 ) ) ;
#27039=FACE_OUTER_BOUND ( 'NONE', #11703, .T. ) ;
#27088=CARTESIAN_POINT ( 'NONE',  ( 84.88357813082512848, -2.741221277476444396, 1.873788409402975530 ) ) ;
#27091=CARTESIAN_POINT ( 'NONE',  ( 101.6960370908956008, -2.521493381538000733, 3.387663558704466116 ) ) ;
#27092=ORIENTED_EDGE ( 'NONE', *, *, #32404, .T. ) ;
#27100=CARTESIAN_POINT ( 'NONE',  ( 28.69354884964465668, -5.617738173989101469, -3.996604665426794156 ) ) ;
#27114=ORIENTED_EDGE ( 'NONE', *, *, #32404, .F. ) ;
#27117=EDGE_CURVE ( 'NONE', #11534, #7768, #8705, .T. ) ;
#27150=CARTESIAN_POINT ( 'NONE',  ( 101.8275707284721250, -4.415545041187804109, 3.393491412270330354 ) ) ;
#27158=CARTESIAN_POINT ( 'NONE',  ( 102.5829460782277351, -0.8583298743146008380, -2.713652344655543391 ) ) ;
#27181=CARTESIAN_POINT ( 'NONE',  ( 28.67239840559955866, -6.439901994755928172, -4.275175838857114385 ) ) ;
#27212=B_SPLINE_CURVE_WITH_KNOTS ( 'NONE', 3,
 ( #24007, #20869, #13659, #23862, #8173, #8331, #8477, #970, #18377, #3160 ),
 .UNSPECIFIED., .F., .F.,
 ( 4, 2, 2, 2, 4 ),
 ( 0.000000000000000000, 0.0003410363541725902007, 0.0006820727083451804014, 0.001023109062517770602, 0.001364145416690360803 ),
 .UNSPECIFIED. ) ;
#27216=CARTESIAN_POINT ( 'NONE',  ( 18.75900454161397590, -5.871068286376763368, 4.006107076242098053 ) ) ;
#27253=CARTESIAN_POINT ( 'NONE',  ( 101.6700243166665842, -2.146915903803417791, 2.784837706280533620 ) ) ;
#27263=CARTESIAN_POINT ( 'NONE',  ( 18.86043735579395886, -4.737252997097608720, -3.995336671762878211 ) ) ;
#27266=ORIENTED_EDGE ( 'NONE', *, *, #29875, .F. ) ;
#27271=FACE_OUTER_BOUND ( 'NONE', #4054, .T. ) ;
#27293=AXIS2_PLACEMENT_3D ( 'NONE', #27008, #19812, #14936 ) ;
#27294=CARTESIAN_POINT ( 'NONE',  ( 101.6199812346112878, -1.426307971359241256, -1.526432238268092823 ) ) ;
#27317=CARTESIAN_POINT ( 'NONE',  ( 102.2517087015684893, -1.537876043683827909, -1.873789182642617401 ) ) ;
#27322=CARTESIAN_POINT ( 'NONE',  ( 23.57316428367674277, -9.051964865549241068, 0.07017451552781736601 ) ) ;
#27362=CARTESIAN_POINT ( 'NONE',  ( 69.04806619055770511, -5.668245219703699433, -4.312042181587000478 ) ) ;
#27379=CARTESIAN_POINT ( 'NONE',  ( 101.6506736443863161, -1.868271036809460384, -2.336400895661424393 ) ) ;
#27383=DIRECTION ( 'NONE',  ( -0.9960221812693187404, 0.08910563629484180570, 0.000000000000000000 ) ) ;
#27391=EDGE_CURVE ( 'NONE', #15472, #12104, #424, .T. ) ;
#27405=CARTESIAN_POINT ( 'NONE',  ( 69.07005235690151324, -6.108409966930705259, 4.006107570159479714 ) ) ;
#27440=CARTESIAN_POINT ( 'NONE',  ( 23.86142584456326432, -3.703306447638166077, 1.529339877387915214 ) ) ;
#27444=VERTEX_POINT ( 'NONE', #8280 ) ;
#27454=CARTESIAN_POINT ( 'NONE',  ( 69.01345486998194190, -4.974821740502390455, -4.001041175463363686 ) ) ;
#27458=CARTESIAN_POINT ( 'NONE',  ( 102.9705908278152293, -6.440317834495088434, -1.915219082070897638 ) ) ;
#27467=ORIENTED_EDGE ( 'NONE', *, *, #31643, .F. ) ;
#27480=B_SPLINE_CURVE_WITH_KNOTS ( 'NONE', 3,
 ( #7866, #5197, #3039, #15542, #23397, #10 ),
 .UNSPECIFIED., .F., .F.,
 ( 4, 2, 4 ),
 ( 0.009531916414662763848, 0.5047659582073313889, 1.000000000000000000 ),
 .UNSPECIFIED. ) ;
#27500=CARTESIAN_POINT ( 'NONE',  ( 102.9885081044300534, -6.698322160490901567, 0.07017451552781736601 ) ) ;
#27508=PLANE ( 'NONE',  #5337 ) ;
#27510=CARTESIAN_POINT ( 'NONE',  ( 84.37491783462850492, -2.359815117480457136, 0.07017451550799885807 ) ) ;
#27531=CARTESIAN_POINT ( 'NONE',  ( 28.66539030321571602, -6.714659430093917081, -4.074610069486789499 ) ) ;
#27549=UNCERTAINTY_MEASURE_WITH_UNIT (LENGTH_MEASURE( 1.000000000000000082E-05 ), #10458, 'distance_accuracy_value', 'NONE');
#27557=CARTESIAN_POINT ( 'NONE',  ( 41.43929652434211164, -5.500819839281755996, -5.695980980372493008 ) ) ;
#27566=CARTESIAN_POINT ( 'NONE',  ( 102.4230146827279668, -3.995787599048658656, 3.999773674144124769 ) ) ;
#27581=CARTESIAN_POINT ( 'NONE',  ( 102.4237878418678633, -3.999739124949584834, -3.993434327387568317 ) ) ;
#27594=CARTESIAN_POINT ( 'NONE',  ( 23.85260150831978265, -3.857138523333644375, 1.873789191099454410 ) ) ;
#27607=CARTESIAN_POINT ( 'NONE',  ( 54.94622396149055277, -5.386472726642053566, -4.033870040937042489 ) ) ;
#27612=CARTESIAN_POINT ( 'NONE',  ( 102.9361373302715918, -5.944196040818416016, -2.713652344655542059 ) ) ;
#27640=ORIENTED_EDGE ( 'NONE', *, *, #20957, .T. ) ;
#27664=CARTESIAN_POINT ( 'NONE',  ( 102.8074457324386515, -4.091069046465106496, 5.695980980372492120 ) ) ;
#27685=EDGE_LOOP ( 'NONE', ( #27114, #5169, #24384, #27640 ) ) ;
#27706=ORIENTED_EDGE ( 'NONE', *, *, #11753, .F. ) ;
#27711=CARTESIAN_POINT ( 'NONE',  ( 18.75856847572524444, -5.875942627837241972, 3.998506281399210049 ) ) ;
#27713=CARTESIAN_POINT ( 'NONE',  ( 18.99198631684116378, -3.266799627756511004, -1.526432259289659532 ) ) ;
#27746=CARTESIAN_POINT ( 'NONE',  ( 40.72654494865490449, -4.620392906571557212, 2.184955499781490840 ) ) ;
#27756=CARTESIAN_POINT ( 'NONE',  ( 28.69317175488845351, -5.632308185119928368, -4.018750267688441902 ) ) ;
#27768=ADVANCED_FACE ( 'NONE', ( #16689 ), #32450, .T. ) ;
#27824=CARTESIAN_POINT ( 'NONE',  ( 29.11693253002209403, -8.303828435806185126, 0.02339150517593243869 ) ) ;
#27826=CARTESIAN_POINT ( 'NONE',  ( 101.6022419886208468, -1.170867242066748304, 0.07017451550800647697 ) ) ;
#27893=CARTESIAN_POINT ( 'NONE',  ( 69.06169492441865998, -5.941118961410190913, 4.185348026735250748 ) ) ;
#27930=CARTESIAN_POINT ( 'NONE',  ( 102.2233072702346277, -1.127920370132900807, 0.07017451552782195956 ) ) ;
#27931=CARTESIAN_POINT ( 'NONE',  ( 18.68265047573912341, -6.724553502642427461, 4.522129901861162260 ) ) ;
#27943=CARTESIAN_POINT ( 'NONE',  ( 28.69326080697081593, -5.628867125850868014, -4.013697994475298181 ) ) ;
#28003=CARTESIAN_POINT ( 'NONE',  ( 48.01729800609908949, -4.703650321870251894, -4.522129901861162260 ) ) ;
#28014=CARTESIAN_POINT ( 'NONE',  ( 29.27523314209665628, -3.695744416148424971, 0.02339150516272637745 ) ) ;
#28033=B_SPLINE_CURVE_WITH_KNOTS ( 'NONE', 3,
 ( #17519, #17875, #9849, #27713, #4821, #25546 ),
 .UNSPECIFIED., .F., .F.,
 ( 4, 2, 4 ),
 ( 0.000000000000000000, 0.001111101127397922479, 0.002222202254795844958 ),
 .UNSPECIFIED. ) ;
#28038=CARTESIAN_POINT ( 'NONE',  ( 23.57316428367446193, -9.051964865574909425, 0.07017451552781803215 ) ) ;
#28068=CARTESIAN_POINT ( 'NONE',  ( 69.06756016430726675, -6.058526890254189112, 4.073742241457220636 ) ) ;
#28082=FACE_OUTER_BOUND ( 'NONE', #23295, .T. ) ;
#28098=CARTESIAN_POINT ( 'NONE',  ( 18.96091535642496240, -3.614110606601101949, 2.184956778829998836 ) ) ;
#28099=CARTESIAN_POINT ( 'NONE',  ( 85.20563808598696198, -3.194259795296082949, 4.522129901861162260 ) ) ;
#28102=ORIENTED_EDGE ( 'NONE', *, *, #7967, .T. ) ;
#28104=CARTESIAN_POINT ( 'NONE',  ( 40.87775850016843293, -5.753518027302250815, -4.001040184496583052 ) ) ;
#28136=CARTESIAN_POINT ( 'NONE',  ( 48.09670199522223299, -9.430894477028838097, 0.07017451552781736601 ) ) ;
#28158=CARTESIAN_POINT ( 'NONE',  ( 69.12694021457090798, -7.241784863855947663, 2.184957268890977300 ) ) ;
#28162=CARTESIAN_POINT ( 'NONE',  ( 41.20585001718148277, -8.497180311781159290, -0.07017451552783579571 ) ) ;
#28165=CARTESIAN_POINT ( 'NONE',  ( 41.43709133142961321, -4.769546740945158625, 4.522129901861162260 ) ) ;
#28171=CARTESIAN_POINT ( 'NONE',  ( 18.75828436641558028, -5.879118399717574661, -3.993434336035625254 ) ) ;
#28173=CARTESIAN_POINT ( 'NONE',  ( 69.09268213438591033, -2.232183665269761086, -0.07017451552781628354 ) ) ;
#28174=( NAMED_UNIT ( * ) PLANE_ANGLE_UNIT ( ) SI_UNIT ( $, .RADIAN. ) );
#28179=CARTESIAN_POINT ( 'NONE',  ( 18.60402535543785518, -7.603424548862136589, 0.07017451552781736601 ) ) ;
#28187=CARTESIAN_POINT ( 'NONE',  ( 29.21519671786122885, -8.552672223064927692, 2.713652344655544724 ) ) ;
#28195=CARTESIAN_POINT ( 'NONE',  ( 23.62691144362026563, -7.794821506207252781, -1.529339877372910550 ) ) ;
#28217=CARTESIAN_POINT ( 'NONE',  ( 85.02775175690295839, -5.073181109254185195, 4.150065216364585474 ) ) ;
#28231=CARTESIAN_POINT ( 'NONE',  ( 18.68265047573912341, -6.724553502642427461, -4.522129901861164036 ) ) ;
#28242=CARTESIAN_POINT ( 'NONE',  ( 102.5437075123491866, -5.726773290143885475, 0.07017451552782749680 ) ) ;
#28243=ORIENTED_EDGE ( 'NONE', *, *, #11320, .T. ) ;
#28244=CARTESIAN_POINT ( 'NONE',  ( 84.41210159610582764, -2.963446145457933945, 2.184954676747139057 ) ) ;
#28247=CARTESIAN_POINT ( 'NONE',  ( 102.6609843814833027, -1.982062027707615970, 4.522129901861162260 ) ) ;
#28252=CARTESIAN_POINT ( 'NONE',  ( 40.87896744413788497, -5.974071964835635740, -4.215290092872233885 ) ) ;
#28260=CARTESIAN_POINT ( 'NONE',  ( 102.9885081044300676, -6.698322160490901567, -1.010822989962099960 ) ) ;
#28269=CARTESIAN_POINT ( 'NONE',  ( 18.64036474505168428, -7.197223105181163483, -1.868788737152627277 ) ) ;
#28293=CARTESIAN_POINT ( 'NONE',  ( 41.44907012423725234, -8.741883605793594469, 2.713652344655544724 ) ) ;
#28306=VECTOR ( 'NONE', #23783, 1000.000000000000000 ) ;
#28315=CARTESIAN_POINT ( 'NONE',  ( 54.99820130842444144, -7.257205178600759865, 2.787782628536179530 ) ) ;
#28318=CARTESIAN_POINT ( 'NONE',  ( 101.6022419886208610, -1.170867242066747416, 0.07017451552782490165 ) ) ;
#28346=CARTESIAN_POINT ( 'NONE',  ( 85.49734435724781179, -7.913007294147517356, 1.010822989962089746 ) ) ;
#28371=EDGE_CURVE ( 'NONE', #32072, #7869, #11746, .T. ) ;
#28378=CARTESIAN_POINT ( 'NONE',  ( 40.87556030650695504, -5.373140178142064904, -3.390607986867075763 ) ) ;
#28386=CARTESIAN_POINT ( 'NONE',  ( 54.97236717404587836, -6.331065523736658207, 4.185347662761127907 ) ) ;
#28405=CARTESIAN_POINT ( 'NONE',  ( 29.20398424897172873, -7.702373504154283346, -2.184956341310761996 ) ) ;
#28414=AXIS2_PLACEMENT_3D ( 'NONE', #17919, #12876, #23408 ) ;
#28417=LINE ( 'NONE', #5529, #4957 ) ;
#28421=CARTESIAN_POINT ( 'NONE',  ( 41.35698357845725326, -8.446179956401751454, 0.8105618903072371317 ) ) ;
#28437=CARTESIAN_POINT ( 'NONE',  ( 69.04182551546352897, -5.543251471596328805, -4.312042181584450518 ) ) ;
#28446=CARTESIAN_POINT ( 'NONE',  ( 23.57316428367446193, -9.051964865574909425, -0.07017451552783579571 ) ) ;
#28478=DIRECTION ( 'NONE',  ( -0.08910563629484158366, -0.9960221812693186294, 0.000000000000000000 ) ) ;
#28498=CARTESIAN_POINT ( 'NONE',  ( 18.74163570027171843, -6.065217073546690152, 3.693462925058700552 ) ) ;
#28505=CARTESIAN_POINT ( 'NONE',  ( 35.28555349212377479, -7.422113525903523801, 2.787782628857160105 ) ) ;
#28514=CARTESIAN_POINT ( 'NONE',  ( 29.35001421184127324, -4.582605737176274729, 4.522129901861162260 ) ) ;
#28567=CARTESIAN_POINT ( 'NONE',  ( 69.05921145838347286, -5.891398902068986310, 4.215290682806994482 ) ) ;
#28581=CARTESIAN_POINT ( 'NONE',  ( 35.29143477761605396, -7.046680052073756251, -3.390608481277731734 ) ) ;
#28593=CARTESIAN_POINT ( 'NONE',  ( 35.27024661284173845, -8.402227462205928532, 0.07017451552782133506 ) ) ;
#28604=CARTESIAN_POINT ( 'NONE',  ( 54.94911284525054640, -5.490851268031983423, -4.150065907156753831 ) ) ;
#28610=CARTESIAN_POINT ( 'NONE',  ( 48.09235817783085309, -9.172289267036324745, -1.915219082070897638 ) ) ;
#28664=CARTESIAN_POINT ( 'NONE',  ( 23.80135741154357731, -5.059951201419131017, 5.695980980372492120 ) ) ;
#28675=CARTESIAN_POINT ( 'NONE',  ( 19.10390797508228999, -2.015740111943971957, -1.010822989962086416 ) ) ;
#28683=CARTESIAN_POINT ( 'NONE',  ( 54.90142980600692368, -3.782945109527315442, -1.169950777188108137 ) ) ;
#28692=B_SPLINE_CURVE_WITH_KNOTS ( 'NONE', 3,
 ( #18210, #22899, #15718, #26073, #25419, #349, #15862, #670 ),
 .UNSPECIFIED., .F., .F.,
 ( 4, 2, 2, 4 ),
 ( 0.009544196576262381146, 0.5047720982881314100, 0.7523860491440657050, 1.000000000000000000 ),
 .UNSPECIFIED. ) ;
#28696=CARTESIAN_POINT ( 'NONE',  ( 29.19213769712790096, -8.050053894908174357, -1.529339505921241349 ) ) ;
#28702=CARTESIAN_POINT ( 'NONE',  ( 84.94207106226072312, -3.684213880880722769, 3.390607676399204795 ) ) ;
#28710=CARTESIAN_POINT ( 'NONE',  ( 68.97545755171863391, -4.219822329608945211, -2.787783122615425935 ) ) ;
#28714=CARTESIAN_POINT ( 'NONE',  ( 18.77836082091593894, -5.654703931404403860, 4.215290389441141095 ) ) ;
#28715=EDGE_CURVE ( 'NONE', #1346, #4533, #21775, .T. ) ;
#28727=VERTEX_POINT ( 'NONE', #21263 ) ;
#28735=B_SPLINE_CURVE_WITH_KNOTS ( 'NONE', 3,
 ( #30135, #19241, #14054, #11704, #27091, #19737, #17042, #27253, #4369, #14551 ),
 .UNSPECIFIED., .F., .F.,
 ( 4, 3, 3, 4 ),
 ( 0.000000000000000000, 0.0005352520061641845642, 0.001070504012328367827, 0.002130599830188110912 ),
 .UNSPECIFIED. ) ;
#28738=CARTESIAN_POINT ( 'NONE',  ( 69.15470699321893733, -7.794592769514708586, 0.8105619180563019555 ) ) ;
#28767=CARTESIAN_POINT ( 'NONE',  ( 29.11693253002209758, -8.303828435806185126, 0.07017451552781737989 ) ) ;
#28778=CARTESIAN_POINT ( 'NONE',  ( 18.60402535543785518, -7.603424548862136589, -0.07017451552783579571 ) ) ;
#28788=CARTESIAN_POINT ( 'NONE',  ( 68.65514544479340486, -4.985459736530871488, 3.993435577424459648 ) ) ;
#28798=CARTESIAN_POINT ( 'NONE',  ( 101.9216173105994443, -5.769792427975428240, -0.07017451552783622593 ) ) ;
#28811=CARTESIAN_POINT ( 'NONE',  ( 68.56906952848856918, -3.255983411059098831, 0.07017451552782104363 ) ) ;
#28835=CARTESIAN_POINT ( 'NONE',  ( 84.85832005755729313, -2.331047133796639859, -0.07017451552781768520 ) ) ;
#28844=CARTESIAN_POINT ( 'NONE',  ( 41.35669399755376929, -8.343390166152927279, -1.169951067574412473 ) ) ;
#28863=CARTESIAN_POINT ( 'NONE',  ( 18.86054332783516330, -4.736068442360130248, -3.993434336035624366 ) ) ;
#28870=CARTESIAN_POINT ( 'NONE',  ( 102.3595522875203159, -3.079674301855471974, 4.215290384276481284 ) ) ;
#28884=CARTESIAN_POINT ( 'NONE',  ( 54.99820130842492460, -7.257205178588800543, -2.787782628555286468 ) ) ;
#28901=CARTESIAN_POINT ( 'NONE',  ( 55.02400815819125768, -8.185693696756606741, 0.8105616793101843021 ) ) ;
#28902=AXIS2_PLACEMENT_3D ( 'NONE', #16260, #18767, #18601 ) ;
#28911=CARTESIAN_POINT ( 'NONE',  ( 54.97716868250573441, -6.504553498923070443, 3.996604662709783540 ) ) ;
#28940=CARTESIAN_POINT ( 'NONE',  ( 18.70785785862773665, -6.442785551927881826, -3.084862407554554320 ) ) ;
#28945=B_SPLINE_SURFACE_WITH_KNOTS ( 'NONE', 3, 3, ( 
 ( #86, #10276, #20495, #2446, #7781, #28162, #2269, #5264, #15437, #12946 ),
 ( #10446, #23163, #32871, #30861, #9939, #17314, #24982, #2093, #20153, #30349 ),
 ( #22484, #32699, #17618, #9779, #20001, #30198, #17460, #27824, #12614, #12777 ),
 ( #17991, #22834, #4962, #15145, #25667, #20170, #15457, #2786, #25354, #28179 ) ),
 .UNSPECIFIED., .F., .F., .F.,
 ( 4, 4 ),
 ( 4, 3, 3, 4 ),
 ( -1.162439711433475187E-14, 1.000000000000000000 ),
 ( 0.009524646911531629151, 0.5047623234557657712, 0.7523811617278828301, 1.000000000000000000 ),
 .UNSPECIFIED. ) ;
#28989=CARTESIAN_POINT ( 'NONE',  ( 35.29731606331253602, -6.671246578258705817, 3.993434333679761306 ) ) ;
#29020=CARTESIAN_POINT ( 'NONE',  ( 68.93909985280586739, -3.497255374392172822, -1.529340295388946336 ) ) ;
#29031=CARTESIAN_POINT ( 'NONE',  ( 55.02400815819124347, -8.185693696756027649, -0.8105616793142609300 ) ) ;
#29052=CARTESIAN_POINT ( 'NONE',  ( 28.69355067552991656, -5.615744008499413908, -3.993434336023910625 ) ) ;
#29058=CARTESIAN_POINT ( 'NONE',  ( 54.96823639739091760, -6.181812932795780924, 4.275175837987727157 ) ) ;
#29117=CARTESIAN_POINT ( 'NONE',  ( 18.67456084474389399, -6.814979340958942977, -2.484925321738187698 ) ) ;
#29154=VERTEX_POINT ( 'NONE', #15296 ) ;
#29164=EDGE_CURVE ( 'NONE', #6888, #19163, #13766, .T. ) ;
#29172=CARTESIAN_POINT ( 'NONE',  ( 35.34214449212195319, -3.792788106923375757, -0.07017451552787916380 ) ) ;
#29182=CARTESIAN_POINT ( 'NONE',  ( 23.61515526891511740, -8.000136145882661864, -0.8105616806143508546 ) ) ;
#29184=EDGE_CURVE ( 'NONE', #20812, #2621, #1426, .T. ) ;
#29203=CARTESIAN_POINT ( 'NONE',  ( 40.88087200079529282, -6.322651088349340753, 4.312042181584448741 ) ) ;
#29205=CARTESIAN_POINT ( 'NONE',  ( 18.85216891279196361, -4.829677595303946802, -4.112224495641408240 ) ) ;
#29218=B_SPLINE_SURFACE_WITH_KNOTS ( 'NONE', 3, 3, ( 
 ( #21186, #30619, #25061, #15029, #25417, #15364, #12543 ),
 ( #25570, #28702, #12849, #2525, #7857, #20579, #12365 ),
 ( #30279, #7512, #13471, #30432, #806, #25248, #10369 ),
 ( #22584, #2370, #22747, #20233, #6642, #18508, #32953 ) ),
 .UNSPECIFIED., .F., .F., .F.,
 ( 4, 4 ),
 ( 4, 3, 4 ),
 ( -7.485815332815247898E-12, 1.000000000000005551 ),
 ( 0.003594141869010686677, 0.5017970709347674418, 1.000000000000524247 ),
 .UNSPECIFIED. ) ;
#29236=CARTESIAN_POINT ( 'NONE',  ( 29.20401286873546809, -7.702374816464193863, 2.184956341613425224 ) ) ;
#29241=B_SPLINE_CURVE_WITH_KNOTS ( 'NONE', 3,
 ( #22180, #30212, #9611, #17141, #24995, #12474, #14646, #32888, #20168, #4960 ),
 .UNSPECIFIED., .F., .F.,
 ( 4, 2, 2, 2, 4 ),
 ( 0.000000000000000000, 0.0003410365069687240733, 0.0006820730139374481466, 0.001023109520906172274, 0.001364146027874896293 ),
 .UNSPECIFIED. ) ;
#29242=CARTESIAN_POINT ( 'NONE',  ( 102.4231811201833438, -3.998190225786205421, 3.995970699063716491 ) ) ;
#29264=CARTESIAN_POINT ( 'NONE',  ( 18.69120935168668041, -6.628882446443490117, -2.784893864646371231 ) ) ;
#29282=CARTESIAN_POINT ( 'NONE',  ( 54.94553969879451927, -5.361749600163809859, -3.997238534717083347 ) ) ;
#29295=CARTESIAN_POINT ( 'NONE',  ( 18.58227844715246135, -7.846511338401735536, -2.713652344655542947 ) ) ;
#29297=CARTESIAN_POINT ( 'NONE',  ( 47.93076651534872923, -6.701564465771713941, 3.993434086975188979 ) ) ;
#29314=CARTESIAN_POINT ( 'NONE',  ( 85.13613392229179055, -2.069934983084471103, -2.713652344655540727 ) ) ;
#29323=CARTESIAN_POINT ( 'NONE',  ( 54.89716490669064797, -3.628845007888692020, -0.07017451552781811541 ) ) ;
#29327=CARTESIAN_POINT ( 'NONE',  ( 101.8146265438530520, -4.229152002780746322, 3.693462844207877627 ) ) ;
#29356=EDGE_CURVE ( 'NONE', #7768, #1159, #4587, .T. ) ;
#29358=CARTESIAN_POINT ( 'NONE',  ( 40.87800967743321934, -5.799281926994868996, 4.074609548159814132 ) ) ;
#29360=CARTESIAN_POINT ( 'NONE',  ( 40.87796467563064340, -5.791092821954919145, -4.053847216751194971 ) ) ;
#29370=ORIENTED_EDGE ( 'NONE', *, *, #15284, .T. ) ;
#29405=ORIENTED_EDGE ( 'NONE', *, *, #22049, .F. ) ;
#29437=ADVANCED_FACE ( 'NONE', ( #30682 ), #6530, .T. ) ;
#29438=CARTESIAN_POINT ( 'NONE',  ( 23.87320362639557203, -3.497993740964699949, 0.8105616805983073547 ) ) ;
#29454=CARTESIAN_POINT ( 'NONE',  ( 18.86033062536104055, -4.738446029132363790, -3.997238537406878844 ) ) ;
#29458=CIRCLE ( 'NONE', #5439, 4.999999999999999112 ) ;
#29482=CARTESIAN_POINT ( 'NONE',  ( 18.93617721851659041, -3.890633339435721982, -4.522129901861162260 ) ) ;
#29493=ORIENTED_EDGE ( 'NONE', *, *, #24064, .F. ) ;
#29507=( BOUNDED_SURFACE ( )  B_SPLINE_SURFACE ( 3, 3, ( 
 ( #12072, #22607, #25274, #4560, #17257, #4389, #32819, #14572 ),
 ( #22267, #32637, #24587, #14734, #20107, #29797, #6870, #25087 ),
 ( #24932, #1713, #32478, #30298, #14375, #32146, #9717, #1898 ),
 ( #7374, #29641, #9539, #7226, #19752, #19942, #11911, #17563 ) ),
 .UNSPECIFIED., .F., .F., .F. ) 
 B_SPLINE_SURFACE_WITH_KNOTS ( ( 4, 4 ),
 ( 4, 2, 2, 4 ),
 ( 0.000000000000000000, 1.000000000000000000 ),
 ( 0.000000000000000000, 0.5000000000000000000, 0.7500000000000000000, 1.000000000000000000 ),
 .UNSPECIFIED. ) 
 GEOMETRIC_REPRESENTATION_ITEM ( )  RATIONAL_B_SPLINE_SURFACE ( (
 ( 1.000000000000000000, 1.000000000000000000, 1.000000000000000000, 1.000000000000000000, 1.000000000000000000, 1.000000000000000000, 1.000000000000000000, 1.000000000000000000),
 ( 0.9743068154145673176, 0.9743068154145673176, 0.9743068154145673176, 0.9743068154145673176, 0.9743068154145673176, 0.9743068154145673176, 0.9743068154145673176, 0.9743068154145673176),
 ( 0.9743068154145673176, 0.9743068154145673176, 0.9743068154145673176, 0.9743068154145673176, 0.9743068154145673176, 0.9743068154145673176, 0.9743068154145673176, 0.9743068154145673176),
 ( 1.000000000000000000, 1.000000000000000000, 1.000000000000000000, 1.000000000000000000, 1.000000000000000000, 1.000000000000000000, 1.000000000000000000, 1.000000000000000000) ) ) 
 REPRESENTATION_ITEM ( '' )  SURFACE ( )  );
#29509=CARTESIAN_POINT ( 'NONE',  ( 68.95644445486074403, -3.844730188641327651, -2.184957270837231569 ) ) ;
#29515=CARTESIAN_POINT ( 'NONE',  ( 101.8731863870445267, -5.072399176882428584, 2.336383929218190492 ) ) ;
#29522=EDGE_CURVE ( 'NONE', #1159, #20638, #29458, .T. ) ;
#29541=EDGE_LOOP ( 'NONE', ( #16318, #2335, #11311, #5379, #10669, #29674, #476, #9657, #3938, #12663, #11865, #4769 ) ) ;
#29582=CARTESIAN_POINT ( 'NONE',  ( 23.68064580653238949, -7.171681651382474598, -4.522129901861164036 ) ) ;
#29585=CARTESIAN_POINT ( 'NONE',  ( 55.01406067017558144, -7.826279391975567101, 1.873789188489173307 ) ) ;
#29592=CARTESIAN_POINT ( 'NONE',  ( 18.75835488814835728, -5.878330108280717781, 3.994702635762014342 ) ) ;
#29620=CARTESIAN_POINT ( 'NONE',  ( 47.88260332740732395, -3.822977517009182868, 0.4367665431859983349 ) ) ;
#29630=CARTESIAN_POINT ( 'NONE',  ( 18.86054332783516330, -4.736068442360130248, -3.993434336035624366 ) ) ;
#29635=CARTESIAN_POINT ( 'NONE',  ( 84.96569962550037758, -4.060952333826338467, -3.996603857777809132 ) ) ;
#29641=CARTESIAN_POINT ( 'NONE',  ( 85.08949032934707191, -1.315411135598756553, 0.07017451552782173751 ) ) ;
#29674=ORIENTED_EDGE ( 'NONE', *, *, #7811, .F. ) ;
#29688=CARTESIAN_POINT ( 'NONE',  ( 102.5437075123492292, -5.726773290143885475, -0.07017451552783424140 ) ) ;
#29714=CARTESIAN_POINT ( 'NONE',  ( 85.02810471335169495, -5.078937868683484957, -4.155404232713865831 ) ) ;
#29747=CARTESIAN_POINT ( 'NONE',  ( 28.66426575328085846, -6.758862791617487709, 4.003574682356660475 ) ) ;
#29775=CARTESIAN_POINT ( 'NONE',  ( 102.2517087015678925, -1.537876043683767735, 1.873789182642447537 ) ) ;
#29778=CARTESIAN_POINT ( 'NONE',  ( 18.51491971917342028, -8.599446730134173933, -0.07017451552783579571 ) ) ;
#29791=CARTESIAN_POINT ( 'NONE',  ( 102.3442017738903047, -2.858083093383076090, -3.998506272710563803 ) ) ;
#29797=CARTESIAN_POINT ( 'NONE',  ( 29.40513214801762842, -2.959508727822389940, 1.915219082070892531 ) ) ;
#29836=CARTESIAN_POINT ( 'NONE',  ( 47.89262141173624343, -4.427686077581835633, -2.184956528778913221 ) ) ;
#29867=CARTESIAN_POINT ( 'NONE',  ( 40.88222826850149261, -6.571667082171160246, -4.275175681037933550 ) ) ;
#29875=EDGE_CURVE ( 'NONE', #21989, #24800, #25712, .T. ) ;
#29877=ORIENTED_EDGE ( 'NONE', *, *, #4293, .T. ) ;
#29898=CARTESIAN_POINT ( 'NONE',  ( 85.20563808598666355, -3.194259795296103821, -4.522129901861162260 ) ) ;
#29906=CARTESIAN_POINT ( 'NONE',  ( 102.4228461758059581, -3.993355098355509281, 4.003574673590898136 ) ) ;
#29920=CARTESIAN_POINT ( 'NONE',  ( 18.65791233782715963, -7.001076235476726417, 2.184956778830005497 ) ) ;
#29921=CARTESIAN_POINT ( 'NONE',  ( 23.95058674323829706, -2.449331254355760823, 0.07017451552782173751 ) ) ;
#29949=CARTESIAN_POINT ( 'NONE',  ( 28.69270465004975890, -5.650360225335952613, -4.043900693839809435 ) ) ;
#29969=EDGE_CURVE ( 'NONE', #30917, #14918, #29241, .T. ) ;
#30026=CARTESIAN_POINT ( 'NONE',  ( 41.19430503359171070, -3.886431767412232396, 0.07017451550800558879 ) ) ;
#30056=EDGE_CURVE ( 'NONE', #20812, #5699, #18270, .T. ) ;
#30069=CARTESIAN_POINT ( 'NONE',  ( 101.6637436982523752, -2.056476561060098796, -2.639289249382372304 ) ) ;
#30090=ORIENTED_EDGE ( 'NONE', *, *, #20313, .T. ) ;
#30098=CARTESIAN_POINT ( 'NONE',  ( 28.66443557441545664, -6.752188475680952706, 4.013697994492946286 ) ) ;
#30102=B_SPLINE_CURVE_WITH_KNOTS ( 'NONE', 3,
 ( #6607, #29515, #19137, #11611, #11288, #6763, #1585, #27150, #29327, #6264 ),
 .UNSPECIFIED., .F., .F.,
 ( 4, 3, 3, 4 ),
 ( 0.000000000000000000, 0.0005351973326734097130, 0.001070394665346821161, 0.002130599829429023241 ),
 .UNSPECIFIED. ) ;
#30118=CARTESIAN_POINT ( 'NONE',  ( 41.35220755422948713, -6.766095577561610952, -3.993434768848478367 ) ) ;
#30132=CARTESIAN_POINT ( 'NONE',  ( 47.89262141172610399, -4.427686077581428847, 2.184956528777964202 ) ) ;
#30135=CARTESIAN_POINT ( 'NONE',  ( 101.7221769401408551, -2.897900707893039662, 3.993434276071444078 ) ) ;
#30145=CARTESIAN_POINT ( 'NONE',  ( 18.85875575654547021, -4.756049901768979460, -4.023790192995878812 ) ) ;
#30150=ADVANCED_FACE ( 'NONE', ( #22986 ), #16896, .T. ) ;
#30192=CARTESIAN_POINT ( 'NONE',  ( 48.09670199522223299, -9.430894477028838097, 0.07017451552781736601 ) ) ;
#30198=CARTESIAN_POINT ( 'NONE',  ( 41.20585001718148277, -8.497180311781159290, 0.02339150517593243869 ) ) ;
#30200=CARTESIAN_POINT ( 'NONE',  ( 41.19430503359171780, -3.886431767412232841, -0.07017451552781628354 ) ) ;
#30202=EDGE_CURVE ( 'NONE', #31589, #11659, #13760, .T. ) ;
#30212=CARTESIAN_POINT ( 'NONE',  ( 101.7264006491823949, -2.958721067365122082, -4.091315454812116670 ) ) ;
#30217=CARTESIAN_POINT ( 'NONE',  ( 40.87773210426689019, -5.748708618950156612, 3.993433839950368824 ) ) ;
#30225=APPLICATION_CONTEXT ( 'configuration controlled 3d designs of mechanical parts and assemblies' ) ;
#30234=CARTESIAN_POINT ( 'NONE',  ( 101.6441386174529384, -1.774168274679073454, -2.184956718804114573 ) ) ;
#30255=CARTESIAN_POINT ( 'NONE',  ( 40.88397857810694092, -6.894206476317448207, 3.997238040198453302 ) ) ;
#30259=DIRECTION ( 'NONE',  ( 0.000000000000000000, 0.000000000000000000, -1.000000000000000000 ) ) ;
#30279=CARTESIAN_POINT ( 'NONE',  ( 102.2915521900159206, -2.105775436102748532, 2.787782622540901478 ) ) ;
#30288=CARTESIAN_POINT ( 'NONE',  ( 19.01480233880980819, -3.011762293215293429, -0.07017451552781921176 ) ) ;
#30293=CARTESIAN_POINT ( 'NONE',  ( 54.94574350846487221, -5.369113455210825947, -4.008637379614919283 ) ) ;
#30298=CARTESIAN_POINT ( 'NONE',  ( 47.98568197278773795, -2.821418575600919354, 1.010822989962091301 ) ) ;
#30304=B_SPLINE_CURVE_WITH_KNOTS ( 'NONE', 3,
 ( #724, #16249, #6210, #11064, #31317, #8393, #18589, #28778 ),
 .UNSPECIFIED., .F., .F.,
 ( 4, 2, 2, 4 ),
 ( 0.009524646911531632620, 0.5047623234557656602, 0.7523811617278828301, 1.000000000000000000 ),
 .UNSPECIFIED. ) ;
#30328=CARTESIAN_POINT ( 'NONE',  ( 18.51491971917340607, -8.599446730134173933, -0.07017451552783579571 ) ) ;
#30333=PRODUCT ( 'Part7_handle1Sleeve', 'Part7_handle1Sleeve', '', ( #5805 ) ) ;
#30343=DIRECTION ( 'NONE',  ( 0.04710975479914572550, 0.5265925107009689077, 0.8488115212910427587 ) ) ;
#30349=CARTESIAN_POINT ( 'NONE',  ( 18.60402535543785518, -7.603424548862136589, -0.02339150517595086839 ) ) ;
#30351=CARTESIAN_POINT ( 'NONE',  ( 19.01480233880806381, -3.011762293215138886, 0.02339150516273075936 ) ) ;
#30372=CARTESIAN_POINT ( 'NONE',  ( 101.8797206818349821, -5.166491396337139719, -2.184956718990371805 ) ) ;
#30385=EDGE_CURVE ( 'NONE', #15360, #19057, #3701, .T. ) ;
#30390=ORIENTED_EDGE ( 'NONE', *, *, #15583, .T. ) ;
#30406=CARTESIAN_POINT ( 'NONE',  ( 102.4223857194505882, -3.986708129022342728, 4.013697985697794124 ) ) ;
#30432=CARTESIAN_POINT ( 'NONE',  ( 54.92448458018063917, -4.608697703007766933, 2.787782628545061314 ) ) ;
#30450=CARTESIAN_POINT ( 'NONE',  ( 84.96817173929643729, -4.101265922145543641, -4.053846905880101659 ) ) ;
#30488=CARTESIAN_POINT ( 'NONE',  ( 85.49734435724840864, -7.913007294147472059, -0.07017451552783579571 ) ) ;
#30505=CARTESIAN_POINT ( 'NONE',  ( 18.86894852475868589, -4.642115209765685258, 3.841991646160189955 ) ) ;
#30535=ORIENTED_EDGE ( 'NONE', *, *, #10569, .T. ) ;
#30538=VECTOR ( 'NONE', #14861, 1000.000000000000000 ) ;
#30550=CARTESIAN_POINT ( 'NONE',  ( 41.45135008765517881, -9.497951668093163491, 0.07017451552781803215 ) ) ;
#30555=CARTESIAN_POINT ( 'NONE',  ( 101.7915493539012033, -3.896846208356848695, 4.171867813802681901 ) ) ;
#30589=CARTESIAN_POINT ( 'NONE',  ( 40.88388279378574452, -6.876528161884418289, 4.023789691746774366 ) ) ;
#30619=CARTESIAN_POINT ( 'NONE',  ( 84.96516786084541195, -4.058994088352219087, 3.993433528812682098 ) ) ;
#30641=CARTESIAN_POINT ( 'NONE',  ( 40.87777647240479695, -5.756792757569010988, -4.006106576936585562 ) ) ;
#30661=CARTESIAN_POINT ( 'NONE',  ( 18.62687130938129343, -7.348052634901513613, -1.527295581757700749 ) ) ;
#30682=FACE_OUTER_BOUND ( 'NONE', #14359, .T. ) ;
#30712=CARTESIAN_POINT ( 'NONE',  ( 47.68482864957696421, -3.825617316378856714, -0.02339150518254430253 ) ) ;
#30713=CARTESIAN_POINT ( 'NONE',  ( 18.74780019990317115, -5.996310340153147678, 5.695980980372492120 ) ) ;
#30720=CARTESIAN_POINT ( 'NONE',  ( 85.08949032934708612, -1.315411135598755221, -0.07017451552781628354 ) ) ;
#30736=ADVANCED_BREP_SHAPE_REPRESENTATION ( '', ( #32130, #2865 ), #21519 ) ;
#30743=CARTESIAN_POINT ( 'NONE',  ( 29.18862856207060119, -8.152784366137925787, -1.169950487275103868 ) ) ;
#30761=EDGE_LOOP ( 'NONE', ( #15651, #12558, #11520, #22990 ) ) ;
#30765=CARTESIAN_POINT ( 'NONE',  ( 18.76136331414632252, -5.844701943473404882, 4.043900693813307079 ) ) ;
#30787=EDGE_CURVE ( 'NONE', #18631, #11534, #16684, .T. ) ;
#30797=CARTESIAN_POINT ( 'NONE',  ( 19.03654924710325602, -2.768675503676416572, 2.713652344655542503 ) ) ;
#30799=SHAPE_REPRESENTATION ( 'Part7_handle1Sleeve', ( #2865 ), #21519 ) ;
#30803=CARTESIAN_POINT ( 'NONE',  ( 18.84882253404822094, -4.867083393560534432, -4.150065909464428771 ) ) ;
#30843=EDGE_LOOP ( 'NONE', ( #11983, #27266, #7289, #26568 ) ) ;
#30861=CARTESIAN_POINT ( 'NONE',  ( 54.77277180716814087, -8.244003004416214253, -0.02339150517595086839 ) ) ;
#30892=CARTESIAN_POINT ( 'NONE',  ( 102.8580990270160385, -4.820463887425400884, 4.522129901861162260 ) ) ;
#30908=CARTESIAN_POINT ( 'NONE',  ( 28.71260074195899037, -4.863490077430783209, -2.787782631220622864 ) ) ;
#30912=CARTESIAN_POINT ( 'NONE',  ( 102.4192815113620725, -3.941896998588075185, 4.073741746331570823 ) ) ;
#30917=VERTEX_POINT ( 'NONE', #6021 ) ;
#30926=CARTESIAN_POINT ( 'NONE',  ( 18.69136968068997007, -6.627090290223585534, -2.787782631232023967 ) ) ;
#30945=CARTESIAN_POINT ( 'NONE',  ( 102.7595417042496706, -3.401262957566509204, 3.636029349014984202 ) ) ;
#30946=CARTESIAN_POINT ( 'NONE',  ( 102.3836362560080033, -3.427337902198302366, -4.312042181584450518 ) ) ;
#30952=CARTESIAN_POINT ( 'NONE',  ( 41.45057005843676734, -9.239282957736854485, -1.915219082070897638 ) ) ;
#30976=ORIENTED_EDGE ( 'NONE', *, *, #7811, .T. ) ;
#30981=CARTESIAN_POINT ( 'NONE',  ( 102.9885081044300534, -6.698322160490901567, -0.07017451552783579571 ) ) ;
#31007=CARTESIAN_POINT ( 'NONE',  ( 35.27967220683390082, -7.797546999730709416, 2.184956776445863280 ) ) ;
#31017=ORIENTED_EDGE ( 'NONE', *, *, #7967, .F. ) ;
#31041=VECTOR ( 'NONE', #20520, 1000.000000000000000 ) ;
#31073=CARTESIAN_POINT ( 'NONE',  ( 102.4077201195289319, -3.775001509873114447, 4.215290384257519563 ) ) ;
#31090=B_SPLINE_SURFACE_WITH_KNOTS ( 'NONE', 1, 3, ( 
 ( #28247, #28099, #23558, #10686, #679, #8356, #21081, #18058 ),
 ( #8019, #18406, #25578, #12861, #18552, #10379, #20588, #30797 ) ),
 .UNSPECIFIED., .F., .F., .F.,
 ( 2, 2 ),
 ( 4, 2, 2, 4 ),
 ( 0.000000000000000000, 1.000000000000000000 ),
 ( 0.000000000000000000, 0.5000000000000000000, 0.7500000000000000000, 1.000000000000000000 ),
 .UNSPECIFIED. ) ;
#31093=CARTESIAN_POINT ( 'NONE',  ( 69.12694021457272697, -7.241784863855113663, -2.184957268911293493 ) ) ;
#31103=VECTOR ( 'NONE', #14108, 1000.000000000000000 ) ;
#31125=CARTESIAN_POINT ( 'NONE',  ( 28.69019293160051731, -5.747507130675590048, -4.150065909478398041 ) ) ;
#31150=VECTOR ( 'NONE', #23953, 1000.000000000000000 ) ;
#31169=CARTESIAN_POINT ( 'NONE',  ( 85.45070076415389337, -7.158483446636730640, 2.713652344655544724 ) ) ;
#31188=CARTESIAN_POINT ( 'NONE',  ( 101.6304955275671773, -1.577711174297567354, 1.868788700125552094 ) ) ;
#31191=CARTESIAN_POINT ( 'NONE',  ( 54.98781319022955927, -6.881869368925546127, 3.390608480947486125 ) ) ;
#31220=FACE_OUTER_BOUND ( 'NONE', #30761, .T. ) ;
#31229=CARTESIAN_POINT ( 'NONE',  ( 23.63572006016191906, -7.640988024202735041, -1.873789191057743331 ) ) ;
#31247=CARTESIAN_POINT ( 'NONE',  ( 102.3175034158304300, -2.480357097899213770, -3.390608474937876871 ) ) ;
#31251=CARTESIAN_POINT ( 'NONE',  ( 69.06576509455614143, -6.022595136392056681, 4.112224952814602652 ) ) ;
#31270=CLOSED_SHELL ( 'NONE', ( #14058, #29437, #31840, #4983, #27768, #19668, #30150, #3341, #31830, #4328, #8325, #18579, #19795, #24465, #18741, #19859, #23260, #22763, #20527, #32885, #20732, #24529, #9097, #7980, #4455, #13415, #12457 ) ) ;
#31276=CARTESIAN_POINT ( 'NONE',  ( 18.60402535544292490, -7.603424548862588672, 0.07017451552782096036 ) ) ;
#31288=CARTESIAN_POINT ( 'NONE',  ( 28.68905448306377792, -5.791583630846771413, -4.185347664757491870 ) ) ;
#31317=CARTESIAN_POINT ( 'NONE',  ( 41.20585001718415441, -8.497180311780732964, -0.07017451552784181867 ) ) ;
#31322=ORIENTED_EDGE ( 'NONE', *, *, #29356, .T. ) ;
#31327=CARTESIAN_POINT ( 'NONE',  ( 41.44567272411835290, -7.615257740949710197, -4.522129901861164036 ) ) ;
#31348=CARTESIAN_POINT ( 'NONE',  ( 18.68265047573912341, -6.724553502642427461, -4.522129901861163148 ) ) ;
#31358=B_SPLINE_SURFACE_WITH_KNOTS ( 'NONE', 3, 3, ( 
 ( #28242, #8499, #5686, #18699, #5350, #13340, #28593, #15721, #10679, #31276 ),
 ( #26243, #15864, #8013, #13522, #18548, #23735, #23390, #3525, #3178, #18213 ),
 ( #25926, #21074, #28738, #28901, #3033, #28421, #496, #11025, #8351, #10524 ),
 ( #21224, #6008, #13680, #10375, #5537, #8198, #18399, #23552, #672, #20583 ),
 ( #5829, #7863, #18055, #15536, #25749, #2880, #13046, #23246, #24032, #21377 ),
 ( #23883, #24222, #9150, #29585, #1651, #4323, #19544, #21864, #17008, #14006 ),
 ( #13826, #11354, #8986, #6319, #992, #21557, #31768, #29236, #22051, #1158 ) ),
 .UNSPECIFIED., .F., .F., .F.,
 ( 4, 3, 4 ),
 ( 4, 3, 3, 4 ),
 ( -8.385610576351451352E-15, 0.4999999999999957812, 1.000000000000000000 ),
 ( 0.003581794793000731177, 0.5017908973965004016, 0.7508954486982502008, 1.000000000000000000 ),
 .UNSPECIFIED. ) ;
#31366=CARTESIAN_POINT ( 'NONE',  ( 23.86731473546760540, -3.600650094290393621, -1.169950778968975369 ) ) ;
#31392=CARTESIAN_POINT ( 'NONE',  ( 18.92745801356166169, -3.988096551854396488, -2.787782631232336161 ) ) ;
#31396=CARTESIAN_POINT ( 'NONE',  ( 84.98546029191203388, -4.383222815445155796, 4.275175582421200993 ) ) ;
#31408=CARTESIAN_POINT ( 'NONE',  ( 23.68974245684628244, -6.697273116524492309, -3.390608483637468584 ) ) ;
#31494=CARTESIAN_POINT ( 'NONE',  ( 19.01480233880806381, -3.011762293215139330, 0.07017451552781951707 ) ) ;
#31517=CARTESIAN_POINT ( 'NONE',  ( 84.86779539662992988, -2.484919561747313210, -1.169950239651971646 ) ) ;
#31551=CARTESIAN_POINT ( 'NONE',  ( 54.95446108372983929, -5.684089628153301099, 4.275175838002291506 ) ) ;
#31589=VERTEX_POINT ( 'NONE', #10743 ) ;
#31595=CARTESIAN_POINT ( 'NONE',  ( 28.66415240725487479, -6.763317863709993993, 3.996604665448017624 ) ) ;
#31620=CARTESIAN_POINT ( 'NONE',  ( 47.75999538435724645, -8.435302152663906483, 0.07017451552781736601 ) ) ;
#31643=EDGE_CURVE ( 'NONE', #7869, #23146, #6488, .T. ) ;
#31695=CARTESIAN_POINT ( 'NONE',  ( 84.41210159610484709, -2.963446145442715451, -2.184954676722655087 ) ) ;
#31737=CARTESIAN_POINT ( 'NONE',  ( 85.00835009345571791, -4.756612885545567160, 4.312042181580753031 ) ) ;
#31768=CARTESIAN_POINT ( 'NONE',  ( 35.27971914370861839, -7.797547734959289656, 2.184956776477424700 ) ) ;
#31773=CARTESIAN_POINT ( 'NONE',  ( 102.4232908028732538, -3.999773562718685671, 3.993434327300716458 ) ) ;
#31812=CARTESIAN_POINT ( 'NONE',  ( 18.86018730484229167, -4.740048064891443147, -3.999773682854171675 ) ) ;
#31830=ADVANCED_FACE ( 'NONE', ( #27271 ), #29507, .T. ) ;
#31838=ORIENTED_EDGE ( 'NONE', *, *, #8358, .T. ) ;
#31840=ADVANCED_FACE ( 'NONE', ( #17416 ), #14751, .T. ) ;
#31847=CARTESIAN_POINT ( 'NONE',  ( 101.6022419886208610, -1.170867242066747416, 0.07017451552782490165 ) ) ;
#31857=CARTESIAN_POINT ( 'NONE',  ( 29.34042402277836104, -3.698761498127606462, -0.4367664976603571336 ) ) ;
#31862=CARTESIAN_POINT ( 'NONE',  ( 101.9180142044465356, -5.717908595713207198, 0.8125824202740279389 ) ) ;
#31866=CARTESIAN_POINT ( 'NONE',  ( 55.02542983044661185, -8.237060396196271839, -0.4367666027069878054 ) ) ;
#31868=EDGE_CURVE ( 'NONE', #4598, #24285, #24120, .T. ) ;
#31880=CARTESIAN_POINT ( 'NONE',  ( 68.65514544479461279, -4.985459736524310514, -3.993435577422745908 ) ) ;
#31889=CARTESIAN_POINT ( 'NONE',  ( 28.68776846593492280, -5.841437261391057234, 4.215290389458900222 ) ) ;
#31891=CARTESIAN_POINT ( 'NONE',  ( 54.95788720338054389, -5.807879973315421829, -4.312042181581901445 ) ) ;
#31898=CARTESIAN_POINT ( 'NONE',  ( 18.96091535642496240, -3.614110606601104614, -2.184956778830005053 ) ) ;
#31902=B_SPLINE_SURFACE_WITH_KNOTS ( 'NONE', 3, 3, ( 
 ( #2993, #13293, #13146, #23346, #20692, #452, #26367, #8135, #25688, #3294 ),
 ( #12987, #21019, #10632, #10479, #13631, #18342, #15824, #26032, #31229, #23499 ),
 ( #5789, #610, #10803, #8306, #10977, #8454, #18499, #28696, #28195, #15965 ),
 ( #26186, #13461, #23679, #21179, #18647, #28844, #18008, #30743, #3473, #23833 ),
 ( #945, #11123, #18995, #29031, #3618, #16453, #32020, #6768, #29182, #8790 ),
 ( #1438, #16625, #3770, #31866, #24160, #16309, #27005, #6270, #1771, #26660 ),
 ( #29688, #24469, #9088, #6424, #3953, #19142, #13777, #26519, #19496, #13940 ) ),
 .UNSPECIFIED., .F., .F., .F.,
 ( 4, 3, 4 ),
 ( 4, 3, 3, 4 ),
 ( -5.415659987738848363E-12, 0.4999999999972921660, 1.000000000000000000 ),
 ( 0.003581794793000549898, 0.5017908973965002906, 0.7508954486982502008, 1.000000000000000000 ),
 .UNSPECIFIED. ) ;
#31923=ORIENTED_EDGE ( 'NONE', *, *, #31643, .T. ) ;
#31954=CARTESIAN_POINT ( 'NONE',  ( 54.89858654025085372, -3.680211708401866399, 0.8105616792983024732 ) ) ;
#31966=CARTESIAN_POINT ( 'NONE',  ( 28.69356951698349434, -5.616939729258927372, -3.995336671782978577 ) ) ;
#31986=CARTESIAN_POINT ( 'NONE',  ( 23.68064580653238949, -7.171681651382474598, -4.522129901861164036 ) ) ;
#31988=DIRECTION ( 'NONE',  ( -0.9960221812693187404, 0.08910563629484180570, 0.000000000000000000 ) ) ;
#32020=CARTESIAN_POINT ( 'NONE',  ( 35.27105150273526846, -8.350847396884441665, -0.8105616794696051119 ) ) ;
#32045=CARTESIAN_POINT ( 'NONE',  ( 102.3922829939908183, -3.552157972648799511, 4.312042181580753031 ) ) ;
#32048=CARTESIAN_POINT ( 'NONE',  ( 40.88330980877409360, -6.770793753989999608, -4.155404504729648174 ) ) ;
#32061=CARTESIAN_POINT ( 'NONE',  ( 29.41391112839825794, -2.700987858898180161, 0.07017451552781951707 ) ) ;
#32072=VERTEX_POINT ( 'NONE', #25401 ) ;
#32104=CARTESIAN_POINT ( 'NONE',  ( 47.98568197278774505, -2.821418575600922019, 0.07017451552782173751 ) ) ;
#32121=CARTESIAN_POINT ( 'NONE',  ( 41.34552818480883474, -4.491668296273251038, 2.184957213357078043 ) ) ;
#32130=MANIFOLD_SOLID_BREP ( 'Shell1', #31270 ) ;
#32140=CARTESIAN_POINT ( 'NONE',  ( 28.69357550994990902, -5.616729480415231457, -3.995006647729451466 ) ) ;
#32146=CARTESIAN_POINT ( 'NONE',  ( 29.41391112839824373, -2.700987858903441730, 1.010822989962091301 ) ) ;
#32172=EDGE_CURVE ( 'NONE', #23146, #27444, #17975, .T. ) ;
#32196=ORIENTED_EDGE ( 'NONE', *, *, #29184, .F. ) ;
#32212=B_SPLINE_CURVE_WITH_KNOTS ( 'NONE', 3,
 ( #9354, #12040, #20074, #32104, #12351, #32784, #29921, #1511 ),
 .UNSPECIFIED., .F., .F.,
 ( 4, 2, 2, 4 ),
 ( 0.000000000000000000, 0.5000000000000000000, 0.7500000000000000000, 1.000000000000000000 ),
 .UNSPECIFIED. ) ;
#32238=CARTESIAN_POINT ( 'NONE',  ( 54.96481031291111918, -6.058022586596120362, -4.312042181587000478 ) ) ;
#32270=CARTESIAN_POINT ( 'NONE',  ( 48.01729800609908949, -4.703650321873321438, -4.522129901861162260 ) ) ;
#32279=CARTESIAN_POINT ( 'NONE',  ( 102.4227322578115462, -3.991710622338239034, 4.006107067514854236 ) ) ;
#32303=EDGE_CURVE ( 'NONE', #11796, #25815, #28735, .T. ) ;
#32324=CARTESIAN_POINT ( 'NONE',  ( 54.94550656002158462, -5.360552262008241975, -3.995336669076017255 ) ) ;
#32365=CARTESIAN_POINT ( 'NONE',  ( 18.97818541978548268, -3.421065958672000917, -1.873789191074026306 ) ) ;
#32404=EDGE_CURVE ( 'NONE', #25815, #32480, #13971, .T. ) ;
#32429=CARTESIAN_POINT ( 'NONE',  ( 40.88396986210033646, -6.892597666169408832, 3.999773184966937567 ) ) ;
#32450=( BOUNDED_SURFACE ( )  B_SPLINE_SURFACE ( 3, 3, ( 
 ( #32759, #29898, #1837, #32270, #17363, #9330, #1489, #19542 ),
 ( #9147, #6977, #19874, #4006, #27557, #17184, #6666, #14679 ),
 ( #24880, #14827, #1991, #12164, #25026, #2141, #12321, #24373 ),
 ( #22542, #9836, #20052, #6485, #26899, #14173, #29582, #11665 ) ),
 .UNSPECIFIED., .F., .F., .T. ) 
 B_SPLINE_SURFACE_WITH_KNOTS ( ( 4, 4 ),
 ( 4, 2, 2, 4 ),
 ( 0.000000000000000000, 1.000000000000000000 ),
 ( 0.000000000000000000, 0.5000000000000000000, 0.7500000000000000000, 1.000000000000000000 ),
 .UNSPECIFIED. ) 
 GEOMETRIC_REPRESENTATION_ITEM ( )  RATIONAL_B_SPLINE_SURFACE ( (
 ( 1.000000000000000000, 1.000000000000000000, 1.000000000000000000, 1.000000000000000000, 1.000000000000000000, 1.000000000000000000, 1.000000000000000000, 1.000000000000000000),
 ( 0.6857970438836928917, 0.6857970438836928917, 0.6857970438836928917, 0.6857970438836928917, 0.6857970438836928917, 0.6857970438836928917, 0.6857970438836928917, 0.6857970438836928917),
 ( 0.6857970438836928917, 0.6857970438836928917, 0.6857970438836928917, 0.6857970438836928917, 0.6857970438836928917, 0.6857970438836928917, 0.6857970438836928917, 0.6857970438836928917),
 ( 1.000000000000000000, 1.000000000000000000, 1.000000000000000000, 1.000000000000000000, 1.000000000000000000, 1.000000000000000000, 1.000000000000000000, 1.000000000000000000) ) ) 
 REPRESENTATION_ITEM ( '' )  SURFACE ( )  );
#32459=CARTESIAN_POINT ( 'NONE',  ( 84.87411226249194840, -2.587501188395394003, 1.529339190611904264 ) ) ;
#32462=CARTESIAN_POINT ( 'NONE',  ( 85.49734435724778336, -7.913007294147514692, -0.07017451552783579571 ) ) ;
#32472=CARTESIAN_POINT ( 'NONE',  ( 102.3440911088257792, -2.856485598251504499, -3.995970699071413446 ) ) ;
#32478=CARTESIAN_POINT ( 'NONE',  ( 69.09268213438589612, -2.232183665269758421, 1.010822989962091301 ) ) ;
#32480=VERTEX_POINT ( 'NONE', #3358 ) ;
#32517=CARTESIAN_POINT ( 'NONE',  ( 84.89549059758259375, -2.934676561234151659, -2.184955970506606171 ) ) ;
#32522=CARTESIAN_POINT ( 'NONE',  ( 101.7221769401408551, -2.897900707893039662, 3.993434276071444078 ) ) ;
#32531=CARTESIAN_POINT ( 'NONE',  ( 101.6022419886208468, -1.170867242066748304, 0.02339150516273448555 ) ) ;
#32532=FACE_OUTER_BOUND ( 'NONE', #6037, .T. ) ;
#32537=CARTESIAN_POINT ( 'NONE',  ( 18.58227844715246135, -7.846511338401735536, 2.713652344655544724 ) ) ;
#32551=CARTESIAN_POINT ( 'NONE',  ( 40.88276903863778955, -6.671230418080579483, -4.215290092883790862 ) ) ;
#32556=CARTESIAN_POINT ( 'NONE',  ( 101.7323081545095107, -3.043787674472451688, 4.171847251016090219 ) ) ;
#32587=CARTESIAN_POINT ( 'NONE',  ( 85.03560246333768191, -5.201294972509532322, 3.998505472958077345 ) ) ;
#32618=CARTESIAN_POINT ( 'NONE',  ( 102.2268587688196106, -1.179183864763504230, 0.8105616763793748181 ) ) ;
#32630=CARTESIAN_POINT ( 'NONE',  ( 40.87778564756947475, -5.758464639511137406, -4.008636882573171967 ) ) ;
#32632=AXIS2_PLACEMENT_3D ( 'NONE', #14702, #14342, #22234 ) ;
#32633=ORIENTED_EDGE ( 'NONE', *, *, #27117, .F. ) ;
#32637=CARTESIAN_POINT ( 'NONE',  ( 85.10544820215893935, -1.573551533646333711, 1.915219082070892531 ) ) ;
#32699=CARTESIAN_POINT ( 'NONE',  ( 84.65816297383790356, -6.961284151106942097, 0.02339150517593242135 ) ) ;
#32703=CARTESIAN_POINT ( 'NONE',  ( 23.68064580653238949, -7.171681651382474598, 4.522129901861163148 ) ) ;
#32740=B_SPLINE_CURVE_WITH_KNOTS ( 'NONE', 3,
 ( #28318, #10449, #28811, #5904, #16096, #3436, #20659, #31494 ),
 .UNSPECIFIED., .F., .F.,
 ( 4, 2, 2, 4 ),
 ( 0.009544196576262197265, 0.5047720982881310769, 0.7523860491440654830, 1.000000000000000000 ),
 .UNSPECIFIED. ) ;
#32759=CARTESIAN_POINT ( 'NONE',  ( 102.6609843814833027, -1.982062027707615526, -4.522129901861162260 ) ) ;
#32764=AXIS2_PLACEMENT_3D ( 'NONE', #14123, #24467, #13626 ) ;
#32768=CARTESIAN_POINT ( 'NONE',  ( 85.03520090177219970, -5.194741742402703366, 4.008636570293263368 ) ) ;
#32784=CARTESIAN_POINT ( 'NONE',  ( 29.41391112839824373, -2.700987858903443950, 0.07017451552782173751 ) ) ;
#32804=CARTESIAN_POINT ( 'NONE',  ( 29.34042402276785566, -3.698761498129368164, 0.4367664976601824955 ) ) ;
#32815=CARTESIAN_POINT ( 'NONE',  ( 69.01421513638182148, -4.990059488610206095, -4.023790688807778793 ) ) ;
#32819=CARTESIAN_POINT ( 'NONE',  ( 23.90742340929308085, -3.204431202270363599, 2.713652344655541615 ) ) ;
#32853=EDGE_CURVE ( 'NONE', #32480, #17452, #6824, .T. ) ;
#32871=CARTESIAN_POINT ( 'NONE',  ( 68.79832465278998654, -7.861404707920828905, -0.02339150517595086839 ) ) ;
#32873=CARTESIAN_POINT ( 'NONE',  ( 84.37491783462850492, -2.359815117480457136, 0.02339150516272687358 ) ) ;
#32885=ADVANCED_FACE ( 'NONE', ( #7323 ), #17233, .F. ) ;
#32888=CARTESIAN_POINT ( 'NONE',  ( 101.7915511448668582, -3.896871997815702482, -4.171847251125799794 ) ) ;
#32903=CARTESIAN_POINT ( 'NONE',  ( 101.7974586501933203, -3.981938604915898683, 4.091315454896042425 ) ) ;
#32913=ORIENTED_EDGE ( 'NONE', *, *, #22049, .T. ) ;
#32920=CARTESIAN_POINT ( 'NONE',  ( 23.61632761762281163, -8.296864917633445913, -2.713652344655543391 ) ) ;
#32924=FACE_OUTER_BOUND ( 'NONE', #30843, .T. ) ;
#32928=CARTESIAN_POINT ( 'NONE',  ( 40.88394771555588392, -6.888509962679972176, 4.006106576922047857 ) ) ;
#32953=CARTESIAN_POINT ( 'NONE',  ( 18.96091535642496240, -3.614110606601104614, 2.184956778830005053 ) ) ;
#32969=CARTESIAN_POINT ( 'NONE',  ( 40.87788096477831346, -5.775834591683154606, -4.033869542163018629 ) ) ;
#32995=CARTESIAN_POINT ( 'NONE',  ( 102.9361373302715918, -5.944196040818416016, 2.713652344655542503 ) ) ;
#33010=CARTESIAN_POINT ( 'NONE',  ( 18.86054332783663767, -4.736068442360261699, 3.993434336035624366 ) ) ;
#33021=CARTESIAN_POINT ( 'NONE',  ( 19.01480233880806381, -3.011762293215139330, 0.07017451552781951707 ) ) ;
#33022=CARTESIAN_POINT ( 'NONE',  ( 19.01480233880806381, -3.011762293215139330, -0.07017451552781628354 ) ) ;
#33023=CARTESIAN_POINT ( 'NONE',  ( 69.13057415542958495, -2.987362752442197955, 2.713652344655542503 ) ) ;
#33031=ORIENTED_EDGE ( 'NONE', *, *, #15284, .F. ) ;
#33072=CARTESIAN_POINT ( 'NONE',  ( 23.84310522038038727, -4.329614468550014195, -4.522129901861162260 ) ) ;
#33076=CARTESIAN_POINT ( 'NONE',  ( 40.88380423908032668, -6.862032121010850361, 4.043900193569005985 ) ) ;
#33106=COLOUR_RGB('Deep Blue', 0.66274510, 0.83137255, 0.94901961);
#33107=FILL_AREA_STYLE_COLOUR('',#33106);
#33108=FILL_AREA_STYLE('',(#33107));
#33109=SURFACE_STYLE_FILL_AREA(#33108);
#33110=SURFACE_SIDE_STYLE('',(#33109));
#33111=SURFACE_STYLE_USAGE(.BOTH.,#33110);
#33112=PRESENTATION_STYLE_ASSIGNMENT((#33111));
#33160=STYLED_ITEM('',(#33112),#32130);
#33161=MECHANICAL_DESIGN_GEOMETRIC_PRESENTATION_REPRESENTATION('',(#33160),#21519);
ENDSEC;
END-ISO-10303-21;
